ISO-10303-21;
HEADER;
FILE_DESCRIPTION (('STEP AP214'),
    '1' );
FILE_NAME ('Heavy Perimeter Inertia Flywheel Disk.step',
    '2026-10-24T00:28:05',
    ( '' ),
    ( '' ),
    'SwSTEP 2.0',
    'SolidWorks 2025',
    '' );
FILE_SCHEMA (( 'AUTOMOTIVE_DESIGN' ));
ENDSEC;

DATA;
#11=ORIENTED_EDGE ( 'NONE', *, *, #16208, .F. ) ;
#41=VECTOR ( 'NONE', #20803, 1000.000000000000000 ) ;
#45=VECTOR ( 'NONE', #2410, 999.9999999999998863 ) ;
#55=CARTESIAN_POINT ( 'NONE',  ( -28.68588794268875475, 600.7448905601785327, 0.000000000000000000 ) ) ;
#64=AXIS2_PLACEMENT_3D ( 'NONE', #6317, #12505, #19097 ) ;
#79=ORIENTED_EDGE ( 'NONE', *, *, #12757, .T. ) ;
#83=ORIENTED_EDGE ( 'NONE', *, *, #15392, .F. ) ;
#101=ORIENTED_EDGE ( 'NONE', *, *, #3009, .T. ) ;
#111=CARTESIAN_POINT ( 'NONE',  ( 18.20947592957839589, 585.7448905601785327, 168.5995991907681457 ) ) ;
#120=EDGE_LOOP ( 'NONE', ( #6723, #18593, #5949, #4393 ) ) ;
#129=FACE_OUTER_BOUND ( 'NONE', #19320, .T. ) ;
#138=DIRECTION ( 'NONE',  ( 1.191790137725560488E-16, -1.000000000000000000, -0.000000000000000000 ) ) ;
#142=DIRECTION ( 'NONE',  ( 1.191790137725560488E-16, -1.000000000000000000, -0.000000000000000000 ) ) ;
#144=CARTESIAN_POINT ( 'NONE',  ( -14.31911992702480241, 600.7448905601785327, 19.70857778461545351 ) ) ;
#204=AXIS2_PLACEMENT_3D ( 'NONE', #20322, #335, #6901 ) ;
#210=EDGE_CURVE ( 'NONE', #6677, #9516, #4265, .T. ) ;
#266=CIRCLE ( 'NONE', #20628, 10.00000000000000888 ) ;
#287=ORIENTED_EDGE ( 'NONE', *, *, #20481, .T. ) ;
#289=VERTEX_POINT ( 'NONE', #7390 ) ;
#335=DIRECTION ( 'NONE',  ( -0.000000000000000000, 1.000000000000000000, -0.000000000000000000 ) ) ;
#344=VECTOR ( 'NONE', #10639, 1000.000000000000000 ) ;
#377=DIRECTION ( 'NONE',  ( 1.000000000000000000, 0.000000000000000000, 0.000000000000000000 ) ) ;
#418=PLANE ( 'NONE',  #13705 ) ;
#444=DIRECTION ( 'NONE',  ( 0.000000000000000000, 1.000000000000000000, -0.000000000000000000 ) ) ;
#445=VERTEX_POINT ( 'NONE', #10184 ) ;
#476=CARTESIAN_POINT ( 'NONE',  ( -33.07955326574333554, 585.7448905601785327, -10.74819839862556314 ) ) ;
#492=EDGE_CURVE ( 'NONE', #4291, #6162, #10377, .T. ) ;
#517=CARTESIAN_POINT ( 'NONE',  ( -64.27068722059112815, 600.7448905601785327, -35.12437985717895828 ) ) ;
#518=DIRECTION ( 'NONE',  ( 1.191790137725560488E-16, -1.000000000000000000, -0.000000000000000000 ) ) ;
#519=DIRECTION ( 'NONE',  ( -1.191790137725560488E-16, 1.000000000000000000, 0.000000000000000000 ) ) ;
#522=EDGE_CURVE ( 'NONE', #2119, #5209, #10396, .T. ) ;
#547=PLANE ( 'NONE',  #5292 ) ;
#577=EDGE_CURVE ( 'NONE', #15582, #9825, #9690, .T. ) ;
#598=LINE ( 'NONE', #13897, #14420 ) ;
#622=CARTESIAN_POINT ( 'NONE',  ( -28.68588794268874764, 575.7448905601785327, 0.000000000000000000 ) ) ;
#657=ORIENTED_EDGE ( 'NONE', *, *, #20933, .F. ) ;
#696=DIRECTION ( 'NONE',  ( 1.000000000000000000, 0.000000000000000000, 0.000000000000000000 ) ) ;
#708=EDGE_LOOP ( 'NONE', ( #11246, #4754, #21207, #11052 ) ) ;
#733=EDGE_CURVE ( 'NONE', #15687, #8097, #12465, .T. ) ;
#744=DIRECTION ( 'NONE',  ( -0.8090169943749474513, 0.000000000000000000, -0.5877852522924730261 ) ) ;
#766=ORIENTED_EDGE ( 'NONE', *, *, #15273, .F. ) ;
#775=VECTOR ( 'NONE', #5701, 1000.000000000000000 ) ;
#783=CARTESIAN_POINT ( 'NONE',  ( -5.502341142637721561, 600.7448905601785327, -7.573322868991255952 ) ) ;
#803=AXIS2_PLACEMENT_3D ( 'NONE', #18452, #8919, #7182 ) ;
#808=CARTESIAN_POINT ( 'NONE',  ( 0.000000000000000000, 0.000000000000000000, 0.000000000000000000 ) ) ;
#815=CIRCLE ( 'NONE', #18408, 50.00000000000000000 ) ;
#818=ORIENTED_EDGE ( 'NONE', *, *, #12595, .F. ) ;
#823=CARTESIAN_POINT ( 'NONE',  ( -18.81370552131603091, 600.7448905601785327, 6.112943483001358480 ) ) ;
#827=VERTEX_POINT ( 'NONE', #16139 ) ;
#832=DIRECTION ( 'NONE',  ( 0.000000000000000000, 1.000000000000000000, -0.000000000000000000 ) ) ;
#872=FACE_OUTER_BOUND ( 'NONE', #15854, .T. ) ;
#877=EDGE_LOOP ( 'NONE', ( #2483, #11, #10820, #14178 ) ) ;
#890=DIRECTION ( 'NONE',  ( 0.000000000000000000, 1.000000000000000000, -0.000000000000000000 ) ) ;
#917=DIRECTION ( 'NONE',  ( 0.000000000000000000, 1.000000000000000000, -0.000000000000000000 ) ) ;
#942=CARTESIAN_POINT ( 'NONE',  ( -28.68588794268874409, 600.7448905601785327, 0.000000000000000000 ) ) ;
#977=VECTOR ( 'NONE', #2716, 1000.000000000000114 ) ;
#979=CARTESIAN_POINT ( 'NONE',  ( 158.8141120573112630, 610.7448905601785327, 10.00000000000000888 ) ) ;
#981=ORIENTED_EDGE ( 'NONE', *, *, #5565, .T. ) ;
#987=ORIENTED_EDGE ( 'NONE', *, *, #20806, .F. ) ;
#1023=LINE ( 'NONE', #14216, #41 ) ;
#1052=CARTESIAN_POINT ( 'NONE',  ( -28.68588794268874054, 588.2448905601785327, 0.000000000000000000 ) ) ;
#1069=PLANE ( 'NONE',  #18679 ) ;
#1086=AXIS2_PLACEMENT_3D ( 'NONE', #13564, #20152, #9973 ) ;
#1095=ORIENTED_EDGE ( 'NONE', *, *, #17426, .F. ) ;
#1112=CARTESIAN_POINT ( 'NONE',  ( -8.938426032941704028E-16, 600.7448905601785327, 7.500000000000000000 ) ) ;
#1123=CARTESIAN_POINT ( 'NONE',  ( 146.3141120573112630, 575.7448905601785327, 0.000000000000000000 ) ) ;
#1135=EDGE_LOOP ( 'NONE', ( #11011, #16877 ) ) ;
#1145=CARTESIAN_POINT ( 'NONE',  ( -28.68588794268874409, 600.7448905601785327, -20.00000000000000355 ) ) ;
#1146=ADVANCED_FACE ( 'NONE', ( #17281 ), #1069, .T. ) ;
#1162=VERTEX_POINT ( 'NONE', #13940 ) ;
#1173=DIRECTION ( 'NONE',  ( 0.000000000000000000, 1.000000000000000000, -0.000000000000000000 ) ) ;
#1184=CARTESIAN_POINT ( 'NONE',  ( -6.276925316985670911, 585.7448905601785327, -44.69718552705352721 ) ) ;
#1251=CARTESIAN_POINT ( 'NONE',  ( 18.20947592957839234, 600.7448905601785327, 168.5995991907681457 ) ) ;
#1263=ORIENTED_EDGE ( 'NONE', *, *, #8344, .F. ) ;
#1287=DIRECTION ( 'NONE',  ( 0.000000000000000000, 1.000000000000000000, -0.000000000000000000 ) ) ;
#1306=CARTESIAN_POINT ( 'NONE',  ( -28.68588794268875120, 585.7448905601785327, 0.000000000000000000 ) ) ;
#1353=CARTESIAN_POINT ( 'NONE',  ( -8.938426032941704028E-16, 600.7448905601785327, 7.500000000000000000 ) ) ;
#1393=LINE ( 'NONE', #6036, #14986 ) ;
#1398=ORIENTED_EDGE ( 'NONE', *, *, #9876, .T. ) ;
#1407=CARTESIAN_POINT ( 'NONE',  ( -33.07955326574332133, 585.7448905601785327, 10.74819839862556492 ) ) ;
#1417=ORIENTED_EDGE ( 'NONE', *, *, #5038, .F. ) ;
#1424=AXIS2_PLACEMENT_3D ( 'NONE', #21238, #11062, #9862 ) ;
#1425=CIRCLE ( 'NONE', #2461, 200.0000000000000000 ) ;
#1439=DIRECTION ( 'NONE',  ( 0.8090169943749474513, 0.000000000000000000, 0.5877852522924730261 ) ) ;
#1448=CARTESIAN_POINT ( 'NONE',  ( -33.07955326574333554, 600.7448905601785327, -10.74819839862556314 ) ) ;
#1478=EDGE_CURVE ( 'NONE', #8423, #10551, #19637, .T. ) ;
#1501=ORIENTED_EDGE ( 'NONE', *, *, #1478, .T. ) ;
#1517=DIRECTION ( 'NONE',  ( 1.191790137725560488E-16, -1.000000000000000000, -0.000000000000000000 ) ) ;
#1520=FACE_OUTER_BOUND ( 'NONE', #17038, .T. ) ;
#1567=CARTESIAN_POINT ( 'NONE',  ( -28.68588794268874409, 608.2448905601786464, -20.00000000000000000 ) ) ;
#1585=CARTESIAN_POINT ( 'NONE',  ( -48.68588794268874409, 585.7448905601785327, 2.449293598294706907E-15 ) ) ;
#1606=AXIS2_PLACEMENT_3D ( 'NONE', #144, #11590, #1439 ) ;
#1610=DIRECTION ( 'NONE',  ( 0.000000000000000000, 1.000000000000000000, -0.000000000000000000 ) ) ;
#1627=CIRCLE ( 'NONE', #5407, 20.00000000000000355 ) ;
#1636=FACE_OUTER_BOUND ( 'NONE', #14623, .T. ) ;
#1638=FACE_BOUND ( 'NONE', #1135, .T. ) ;
#1641=AXIS2_PLACEMENT_3D ( 'NONE', #2977, #9555, #19198 ) ;
#1661=ORIENTED_EDGE ( 'NONE', *, *, #1693, .T. ) ;
#1693=EDGE_CURVE ( 'NONE', #5209, #6118, #4155, .T. ) ;
#1706=APPLICATION_CONTEXT ( 'automotive_design' ) ;
#1722=CARTESIAN_POINT ( 'NONE',  ( 158.8141120573112630, 575.7448905601785327, 0.000000000000000000 ) ) ;
#1745=ORIENTED_EDGE ( 'NONE', *, *, #3500, .T. ) ;
#1748=FACE_BOUND ( 'NONE', #6583, .T. ) ;
#1752=ORIENTED_EDGE ( 'NONE', *, *, #20775, .T. ) ;
#1768=DIRECTION ( 'NONE',  ( 0.000000000000000000, 0.000000000000000000, 1.000000000000000000 ) ) ;
#1796=DIRECTION ( 'NONE',  ( -0.3090169943749473402, 0.000000000000000000, -0.9510565162951535312 ) ) ;
#1806=ORIENTED_EDGE ( 'NONE', *, *, #12490, .T. ) ;
#1813=AXIS2_PLACEMENT_3D ( 'NONE', #1052, #21250, #21037 ) ;
#1814=VERTEX_POINT ( 'NONE', #1145 ) ;
#1827=MECHANICAL_DESIGN_GEOMETRIC_PRESENTATION_REPRESENTATION('',(#4219),#20805);
#1837=VECTOR ( 'NONE', #6097, 1000.000000000000000 ) ;
#1838=ORIENTED_EDGE ( 'NONE', *, *, #16152, .T. ) ;
#1851=CIRCLE ( 'NONE', #5281, 50.00000000000000000 ) ;
#1861=DIRECTION ( 'NONE',  ( 0.000000000000000000, 0.000000000000000000, 1.000000000000000000 ) ) ;
#1961=ORIENTED_EDGE ( 'NONE', *, *, #2820, .F. ) ;
#1978=VECTOR ( 'NONE', #2773, 1000.000000000000000 ) ;
#1979=DIRECTION ( 'NONE',  ( 1.191790137725560488E-16, -1.000000000000000000, -0.000000000000000000 ) ) ;
#1981=CARTESIAN_POINT ( 'NONE',  ( 146.1533239063698772, 585.7448905601785327, 7.500000000000000000 ) ) ;
#1988=AXIS2_PLACEMENT_3D ( 'NONE', #4495, #15868, #2663 ) ;
#2026=ADVANCED_FACE ( 'NONE', ( #3292 ), #3499, .T. ) ;
#2034=FACE_OUTER_BOUND ( 'NONE', #10469, .T. ) ;
#2044=ORIENTED_EDGE ( 'NONE', *, *, #7088, .T. ) ;
#2075=CARTESIAN_POINT ( 'NONE',  ( -165.7253922195053519, 600.7448905601785327, -108.8355377051282034 ) ) ;
#2110=CIRCLE ( 'NONE', #3489, 20.00000000000000000 ) ;
#2119=VERTEX_POINT ( 'NONE', #6736 ) ;
#2130=CARTESIAN_POINT ( 'NONE',  ( 18.20947592957834260, 600.7448905601785327, -168.5995991907681173 ) ) ;
#2133=CARTESIAN_POINT ( 'NONE',  ( 158.8141120573112630, 10.52886280891152104, 0.000000000000000000 ) ) ;
#2150=CARTESIAN_POINT ( 'NONE',  ( 146.3141120573112630, 585.7448905601785327, 0.000000000000000000 ) ) ;
#2179=AXIS2_PLACEMENT_3D ( 'NONE', #15173, #18818, #6926 ) ;
#2183=CARTESIAN_POINT ( 'NONE',  ( -28.68588794268875120, 585.7448905601785327, 0.000000000000000000 ) ) ;
#2211=VECTOR ( 'NONE', #13090, 1000.000000000000114 ) ;
#2237=EDGE_CURVE ( 'NONE', #12962, #6677, #21092, .T. ) ;
#2247=ADVANCED_FACE ( 'NONE', ( #1520 ), #3035, .T. ) ;
#2271=EDGE_LOOP ( 'NONE', ( #21027, #16797 ) ) ;
#2282=DIRECTION ( 'NONE',  ( 0.3090169943749471182, -0.000000000000000000, -0.9510565162951537532 ) ) ;
#2292=ORIENTED_EDGE ( 'NONE', *, *, #8145, .F. ) ;
#2309=CIRCLE ( 'NONE', #10225, 175.0000000000000284 ) ;
#2315=DIRECTION ( 'NONE',  ( -0.8090169943749474513, 0.000000000000000000, -0.5877852522924730261 ) ) ;
#2323=VECTOR ( 'NONE', #11187, 1000.000000000000000 ) ;
#2334=CIRCLE ( 'NONE', #15463, 20.00000000000000711 ) ;
#2373=AXIS2_PLACEMENT_3D ( 'NONE', #9376, #17703, #10775 ) ;
#2377=ORIENTED_EDGE ( 'NONE', *, *, #15674, .F. ) ;
#2404=ORIENTED_EDGE ( 'NONE', *, *, #21120, .T. ) ;
#2410=DIRECTION ( 'NONE',  ( 0.3090169943749471182, -0.000000000000000000, -0.9510565162951537532 ) ) ;
#2419=DIRECTION ( 'NONE',  ( 0.000000000000000000, 0.000000000000000000, 1.000000000000000000 ) ) ;
#2425=DIRECTION ( 'NONE',  ( 1.191790137725560488E-16, -1.000000000000000000, -0.000000000000000000 ) ) ;
#2456=ADVANCED_FACE ( 'NONE', ( #11886 ), #16770, .F. ) ;
#2461=AXIS2_PLACEMENT_3D ( 'NONE', #12365, #917, #4252 ) ;
#2483=ORIENTED_EDGE ( 'NONE', *, *, #8756, .T. ) ;
#2499=LINE ( 'NONE', #783, #977 ) ;
#2527=AXIS2_PLACEMENT_3D ( 'NONE', #55, #10190, #377 ) ;
#2530=PLANE ( 'NONE',  #13028 ) ;
#2533=EDGE_LOOP ( 'NONE', ( #12722, #17671, #818, #18378, #1752, #7518, #987, #19029 ) ) ;
#2552=CARTESIAN_POINT ( 'NONE',  ( -165.7253922195053235, 585.7448905601785327, 108.8355377051282176 ) ) ;
#2560=VERTEX_POINT ( 'NONE', #979 ) ;
#2562=EDGE_LOOP ( 'NONE', ( #9288, #20647, #11571, #14040, #16782, #6294, #19627, #4293, #4499, #12669, #13046, #8315, #11460, #12863, #19706, #8488, #3063, #6641, #7418, #12835, #14389 ) ) ;
#2589=VERTEX_POINT ( 'NONE', #12096 ) ;
#2592=ORIENTED_EDGE ( 'NONE', *, *, #8743, .F. ) ;
#2609=ORIENTED_EDGE ( 'NONE', *, *, #10014, .T. ) ;
#2612=ORIENTED_EDGE ( 'NONE', *, *, #5110, .T. ) ;
#2620=DIRECTION ( 'NONE',  ( 0.000000000000000000, 0.000000000000000000, 1.000000000000000000 ) ) ;
#2658=DIRECTION ( 'NONE',  ( 1.191790137725560488E-16, -1.000000000000000000, -0.000000000000000000 ) ) ;
#2663=DIRECTION ( 'NONE',  ( 0.000000000000000000, 0.000000000000000000, 1.000000000000000000 ) ) ;
#2689=VECTOR ( 'NONE', #17263, 1000.000000000000000 ) ;
#2716=DIRECTION ( 'NONE',  ( -0.8090169943749473402, 0.000000000000000000, 0.5877852522924733591 ) ) ;
#2723=EDGE_CURVE ( 'NONE', #11194, #15706, #13945, .T. ) ;
#2759=ORIENTED_EDGE ( 'NONE', *, *, #20663, .F. ) ;
#2773=DIRECTION ( 'NONE',  ( 1.000000000000000000, 0.000000000000000000, 0.000000000000000000 ) ) ;
#2777=EDGE_LOOP ( 'NONE', ( #19575, #2592, #4506, #5910 ) ) ;
#2779=ORIENTED_EDGE ( 'NONE', *, *, #7166, .T. ) ;
#2820=EDGE_CURVE ( 'NONE', #14497, #20490, #3928, .T. ) ;
#2830=ORIENTED_EDGE ( 'NONE', *, *, #16657, .F. ) ;
#2880=FACE_OUTER_BOUND ( 'NONE', #7918, .T. ) ;
#2890=ORIENTED_EDGE ( 'NONE', *, *, #21068, .F. ) ;
#2977=CARTESIAN_POINT ( 'NONE',  ( -28.68588794268875475, 600.7448905601785327, 0.000000000000000000 ) ) ;
#2979=LINE ( 'NONE', #1353, #1837 ) ;
#3003=AXIS2_PLACEMENT_3D ( 'NONE', #2133, #15339, #20298 ) ;
#3009=EDGE_CURVE ( 'NONE', #20997, #1814, #18022, .T. ) ;
#3025=CIRCLE ( 'NONE', #1641, 50.00000000000000000 ) ;
#3035=PLANE ( 'NONE',  #5313 ) ;
#3041=DIRECTION ( 'NONE',  ( -1.191790137725560488E-16, 1.000000000000000000, 0.000000000000000000 ) ) ;
#3063=ORIENTED_EDGE ( 'NONE', *, *, #20806, .T. ) ;
#3081=DIRECTION ( 'NONE',  ( 0.000000000000000000, 0.000000000000000000, 1.000000000000000000 ) ) ;
#3123=CARTESIAN_POINT ( 'NONE',  ( -6.276925316985662029, 585.7448905601785327, 44.69718552705352010 ) ) ;
#3133=CARTESIAN_POINT ( 'NONE',  ( -13.68588794268873521, 548.2448905601784190, 0.000000000000000000 ) ) ;
#3149=DIRECTION ( 'NONE',  ( 1.191790137725560488E-16, -1.000000000000000000, -0.000000000000000000 ) ) ;
#3168=EDGE_CURVE ( 'NONE', #21019, #6223, #9543, .T. ) ;
#3180=CARTESIAN_POINT ( 'NONE',  ( 18.20947592957839234, 600.7448905601785327, 168.5995991907681457 ) ) ;
#3216=CARTESIAN_POINT ( 'NONE',  ( -28.68588794268874409, 608.2448905601786464, -20.00000000000000000 ) ) ;
#3223=DIRECTION ( 'NONE',  ( 0.000000000000000000, 1.000000000000000000, -0.000000000000000000 ) ) ;
#3251=EDGE_LOOP ( 'NONE', ( #19896, #13797, #2612, #9442 ) ) ;
#3292=FACE_OUTER_BOUND ( 'NONE', #877, .T. ) ;
#3304=LINE ( 'NONE', #14993, #13713 ) ;
#3334=ORIENTED_EDGE ( 'NONE', *, *, #14717, .T. ) ;
#3338=ORIENTED_EDGE ( 'NONE', *, *, #2723, .T. ) ;
#3341=AXIS2_PLACEMENT_3D ( 'NONE', #9961, #16580, #1768 ) ;
#3354=VECTOR ( 'NONE', #13359, 1000.000000000000000 ) ;
#3372=EDGE_CURVE ( 'NONE', #7175, #6933, #7250, .T. ) ;
#3390=ORIENTED_EDGE ( 'NONE', *, *, #15256, .T. ) ;
#3404=CARTESIAN_POINT ( 'NONE',  ( -28.68588794268874409, 608.2448905601786464, 0.000000000000000000 ) ) ;
#3437=CYLINDRICAL_SURFACE ( 'NONE', #12222, 200.0000000000000000 ) ;
#3487=ORIENTED_EDGE ( 'NONE', *, *, #13735, .F. ) ;
#3489=AXIS2_PLACEMENT_3D ( 'NONE', #16687, #4772, #16792 ) ;
#3498=SHAPE_DEFINITION_REPRESENTATION ( #16340, #18847 ) ;
#3499=CYLINDRICAL_SURFACE ( 'NONE', #2527, 50.00000000000000000 ) ;
#3500=EDGE_CURVE ( 'NONE', #6477, #2589, #5216, .T. ) ;
#3540=AXIS2_PLACEMENT_3D ( 'NONE', #6271, #3041, #19475 ) ;
#3551=CIRCLE ( 'NONE', #16341, 175.0000000000000284 ) ;
#3595=ORIENTED_EDGE ( 'NONE', *, *, #2237, .F. ) ;
#3612=ADVANCED_FACE ( 'NONE', ( #12454 ), #18829, .F. ) ;
#3620=EDGE_CURVE ( 'NONE', #18564, #7989, #17080, .T. ) ;
#3627=ORIENTED_EDGE ( 'NONE', *, *, #3372, .T. ) ;
#3628=CARTESIAN_POINT ( 'NONE',  ( -165.7253922195052951, 600.7448905601785327, 108.8355377051282176 ) ) ;
#3648=ORIENTED_EDGE ( 'NONE', *, *, #4601, .F. ) ;
#3663=CARTESIAN_POINT ( 'NONE',  ( -28.68588794268875120, 610.7448905601785327, 0.000000000000000000 ) ) ;
#3673=ORIENTED_EDGE ( 'NONE', *, *, #14717, .F. ) ;
#3725=ORIENTED_EDGE ( 'NONE', *, *, #18225, .T. ) ;
#3735=CARTESIAN_POINT ( 'NONE',  ( -48.68588794268874409, 548.2448905601784190, 2.449293598294706513E-15 ) ) ;
#3742=DIRECTION ( 'NONE',  ( 0.8090169943749474513, 0.000000000000000000, 0.5877852522924730261 ) ) ;
#3746=ORIENTED_EDGE ( 'NONE', *, *, #20933, .T. ) ;
#3841=FACE_OUTER_BOUND ( 'NONE', #13554, .T. ) ;
#3857=ADVANCED_FACE ( 'NONE', ( #1636, #20998 ), #6163, .F. ) ;
#3879=VERTEX_POINT ( 'NONE', #14416 ) ;
#3899=DIRECTION ( 'NONE',  ( 0.000000000000000000, 1.000000000000000000, -0.000000000000000000 ) ) ;
#3928=CIRCLE ( 'NONE', #14314, 175.0000000000000284 ) ;
#4038=VECTOR ( 'NONE', #11393, 1000.000000000000000 ) ;
#4042=ADVANCED_BREP_SHAPE_REPRESENTATION ( '', ( #4359, #12794 ), #20056 ) ;
#4051=CIRCLE ( 'NONE', #20287, 175.0000000000000284 ) ;
#4069=ORIENTED_EDGE ( 'NONE', *, *, #15846, .T. ) ;
#4118=ORIENTED_EDGE ( 'NONE', *, *, #7307, .T. ) ;
#4131=CARTESIAN_POINT ( 'NONE',  ( -28.68588794268874054, 608.2448905601786464, 20.00000000000000000 ) ) ;
#4142=ORIENTED_EDGE ( 'NONE', *, *, #16439, .F. ) ;
#4155=LINE ( 'NONE', #5774, #344 ) ;
#4160=DIRECTION ( 'NONE',  ( -0.000000000000000000, -1.000000000000000000, 0.000000000000000000 ) ) ;
#4184=APPLICATION_CONTEXT ( 'automotive_design' ) ;
#4185=EDGE_LOOP ( 'NONE', ( #8234, #2377, #20435, #7883 ) ) ;
#4197=EDGE_CURVE ( 'NONE', #5663, #6477, #7425, .T. ) ;
#4209=CARTESIAN_POINT ( 'NONE',  ( 2.085632741019731137E-15, 575.7448905601785327, 0.000000000000000000 ) ) ;
#4219=STYLED_ITEM('',(#21449),#4359);
#4252=DIRECTION ( 'NONE',  ( 0.000000000000000000, 0.000000000000000000, 1.000000000000000000 ) ) ;
#4262=EDGE_CURVE ( 'NONE', #13474, #18564, #18024, .T. ) ;
#4265=LINE ( 'NONE', #7172, #4839 ) ;
#4274=ADVANCED_FACE ( 'NONE', ( #9589 ), #14586, .F. ) ;
#4291=VERTEX_POINT ( 'NONE', #4825 ) ;
#4293=ORIENTED_EDGE ( 'NONE', *, *, #12135, .T. ) ;
#4304=DIRECTION ( 'NONE',  ( 0.000000000000000000, 0.000000000000000000, 1.000000000000000000 ) ) ;
#4352=FACE_BOUND ( 'NONE', #5166, .T. ) ;
#4359=MANIFOLD_SOLID_BREP ( 'Cut-Extrude11', #5200 ) ;
#4393=ORIENTED_EDGE ( 'NONE', *, *, #14386, .T. ) ;
#4438=AXIS2_PLACEMENT_3D ( 'NONE', #17598, #1173, #14374 ) ;
#4456=DIRECTION ( 'NONE',  ( 0.000000000000000000, 0.000000000000000000, 1.000000000000000000 ) ) ;
#4458=SHAPE_REPRESENTATION_RELATIONSHIP ( 'NONE' , 'NONE' ,  #18847, #4042 ) ;
#4461=CARTESIAN_POINT ( 'NONE',  ( -33.07955326574332133, 600.7448905601785327, 10.74819839862556492 ) ) ;
#4484=ADVANCED_FACE ( 'NONE', ( #18654, #17264, #13808 ), #15545, .F. ) ;
#4492=FACE_OUTER_BOUND ( 'NONE', #9286, .T. ) ;
#4495=CARTESIAN_POINT ( 'NONE',  ( -28.68588794268875475, 600.7448905601785327, 0.000000000000000000 ) ) ;
#4497=VERTEX_POINT ( 'NONE', #20609 ) ;
#4499=ORIENTED_EDGE ( 'NONE', *, *, #17031, .F. ) ;
#4506=ORIENTED_EDGE ( 'NONE', *, *, #3168, .T. ) ;
#4538=AXIS2_PLACEMENT_3D ( 'NONE', #11685, #21311, #1861 ) ;
#4545=DIRECTION ( 'NONE',  ( 1.000000000000000000, 0.000000000000000000, 0.000000000000000000 ) ) ;
#4578=ORIENTED_EDGE ( 'NONE', *, *, #11471, .F. ) ;
#4601=EDGE_CURVE ( 'NONE', #5209, #6223, #6630, .T. ) ;
#4612=ORIENTED_EDGE ( 'NONE', *, *, #18880, .T. ) ;
#4618=FACE_BOUND ( 'NONE', #16556, .T. ) ;
#4641=ADVANCED_FACE ( 'NONE', ( #4492 ), #9352, .T. ) ;
#4671=CARTESIAN_POINT ( 'NONE',  ( 32.47532367400565079, 600.7448905601785327, -163.9643442751439864 ) ) ;
#4713=CIRCLE ( 'NONE', #20967, 50.00000000000000000 ) ;
#4718=CARTESIAN_POINT ( 'NONE',  ( -28.68588794268874409, 600.7448905601785327, 0.000000000000000000 ) ) ;
#4719=EDGE_CURVE ( 'NONE', #11194, #20333, #10390, .T. ) ;
#4722=DIRECTION ( 'NONE',  ( 1.191790137725560488E-16, -1.000000000000000000, -0.000000000000000000 ) ) ;
#4737=ORIENTED_EDGE ( 'NONE', *, *, #1693, .F. ) ;
#4745=VECTOR ( 'NONE', #1979, 1000.000000000000000 ) ;
#4749=CARTESIAN_POINT ( 'NONE',  ( -14.31911992702480774, 585.7448905601785327, -19.70857778461545351 ) ) ;
#4754=ORIENTED_EDGE ( 'NONE', *, *, #7166, .F. ) ;
#4759=FACE_OUTER_BOUND ( 'NONE', #5931, .T. ) ;
#4771=DIRECTION ( 'NONE',  ( 1.000000000000000000, 0.000000000000000000, 0.000000000000000000 ) ) ;
#4772=DIRECTION ( 'NONE',  ( 0.000000000000000000, 1.000000000000000000, 0.000000000000000000 ) ) ;
#4778=EDGE_CURVE ( 'NONE', #15582, #11085, #17685, .T. ) ;
#4818=VECTOR ( 'NONE', #2282, 999.9999999999998863 ) ;
#4825=CARTESIAN_POINT ( 'NONE',  ( 171.3141120573112630, 575.7448905601785327, 0.000000000000000000 ) ) ;
#4839=VECTOR ( 'NONE', #17456, 1000.000000000000000 ) ;
#4878=CARTESIAN_POINT ( 'NONE',  ( -174.5421710038924061, 585.7448905601785327, 96.70028278950401557 ) ) ;
#4909=DIRECTION ( 'NONE',  ( -0.8090169943749474513, 0.000000000000000000, -0.5877852522924730261 ) ) ;
#4939=( NAMED_UNIT ( * ) PLANE_ANGLE_UNIT ( ) SI_UNIT ( $, .RADIAN. ) );
#4961=CARTESIAN_POINT ( 'NONE',  ( -73.08746600497821078, 600.7448905601785327, -22.98912494155474207 ) ) ;
#5014=CARTESIAN_POINT ( 'NONE',  ( -8.685887942688731655, 548.2448905601784190, 0.000000000000000000 ) ) ;
#5015=LINE ( 'NONE', #10195, #18664 ) ;
#5017=CARTESIAN_POINT ( 'NONE',  ( 20.74841189052421697, 600.7448905601785327, 7.500000000000000000 ) ) ;
#5038=EDGE_CURVE ( 'NONE', #1162, #5907, #10513, .T. ) ;
#5054=EDGE_LOOP ( 'NONE', ( #6322, #17971 ) ) ;
#5060=VECTOR ( 'NONE', #7134, 1000.000000000000000 ) ;
#5096=DIRECTION ( 'NONE',  ( -0.000000000000000000, -1.000000000000000000, -0.000000000000000000 ) ) ;
#5100=CARTESIAN_POINT ( 'NONE',  ( -28.68588794268875120, 585.7448905601785327, 0.000000000000000000 ) ) ;
#5110=EDGE_CURVE ( 'NONE', #6162, #4291, #1425, .T. ) ;
#5165=VECTOR ( 'NONE', #11667, 1000.000000000000000 ) ;
#5166=EDGE_LOOP ( 'NONE', ( #16934, #15317 ) ) ;
#5200=CLOSED_SHELL ( 'NONE', ( #2456, #16599, #10713, #4274, #15176, #4484, #20468, #7353, #10531, #6510, #18478, #8194, #18073, #13463, #16844, #14313, #1146, #5645, #15991, #2247, #2026, #3612, #11674, #9859, #8507, #14682, #9340, #6652, #18819, #3857, #4641, #16723, #7685, #18075 ) ) ;
#5202=EDGE_CURVE ( 'NONE', #10415, #10685, #21013, .T. ) ;
#5209=VERTEX_POINT ( 'NONE', #4671 ) ;
#5216=LINE ( 'NONE', #8561, #10162 ) ;
#5232=CARTESIAN_POINT ( 'NONE',  ( -28.68588794268875475, 600.7448905601785327, 0.000000000000000000 ) ) ;
#5244=VERTEX_POINT ( 'NONE', #10941 ) ;
#5256=CARTESIAN_POINT ( 'NONE',  ( -28.68588794268875120, 585.7448905601785327, 0.000000000000000000 ) ) ;
#5271=AXIS2_PLACEMENT_3D ( 'NONE', #14027, #4160, #7507 ) ;
#5281=AXIS2_PLACEMENT_3D ( 'NONE', #6580, #9822, #7878 ) ;
#5284=ORIENTED_EDGE ( 'NONE', *, *, #5335, .F. ) ;
#5292=AXIS2_PLACEMENT_3D ( 'NONE', #4209, #444, #18585 ) ;
#5313=AXIS2_PLACEMENT_3D ( 'NONE', #17739, #9511, #19468 ) ;
#5325=PRODUCT_CONTEXT ( 'NONE', #1706, 'mechanical' ) ;
#5335=EDGE_CURVE ( 'NONE', #20381, #11578, #1023, .T. ) ;
#5344=EDGE_CURVE ( 'NONE', #20997, #11679, #2110, .T. ) ;
#5352=PLANE ( 'NONE',  #9632 ) ;
#5407=AXIS2_PLACEMENT_3D ( 'NONE', #942, #7509, #9460 ) ;
#5416=VECTOR ( 'NONE', #15430, 1000.000000000000000 ) ;
#5424=AXIS2_PLACEMENT_3D ( 'NONE', #9321, #15939, #11158 ) ;
#5527=ORIENTED_EDGE ( 'NONE', *, *, #3620, .F. ) ;
#5565=EDGE_CURVE ( 'NONE', #14938, #13766, #12461, .T. ) ;
#5568=DIRECTION ( 'NONE',  ( -0.3090169943749470072, 0.000000000000000000, 0.9510565162951536422 ) ) ;
#5598=CARTESIAN_POINT ( 'NONE',  ( -8.938426032941704028E-16, 600.7448905601785327, -7.500000000000000000 ) ) ;
#5605=AXIS2_PLACEMENT_3D ( 'NONE', #20957, #13054, #16313 ) ;
#5637=DIRECTION ( 'NONE',  ( -1.000000000000000000, 0.000000000000000000, -0.000000000000000000 ) ) ;
#5645=ADVANCED_FACE ( 'NONE', ( #15814 ), #14082, .T. ) ;
#5652=VECTOR ( 'NONE', #16060, 1000.000000000000000 ) ;
#5663=VERTEX_POINT ( 'NONE', #16124 ) ;
#5672=AXIS2_PLACEMENT_3D ( 'NONE', #1112, #18936, #5637 ) ;
#5674=CARTESIAN_POINT ( 'NONE',  ( -18.81370552131602736, 600.7448905601785327, -6.112943483001347822 ) ) ;
#5693=ORIENTED_EDGE ( 'NONE', *, *, #20663, .T. ) ;
#5701=DIRECTION ( 'NONE',  ( 1.000000000000000000, 0.000000000000000000, 0.000000000000000000 ) ) ;
#5764=PRODUCT ( 'Heavy Perimeter Inertia Flywheel Disk', 'Heavy Perimeter Inertia Flywheel Disk', '', ( #5325 ) ) ;
#5774=CARTESIAN_POINT ( 'NONE',  ( 32.47532367400565079, 600.7448905601785327, -163.9643442751439864 ) ) ;
#5852=CIRCLE ( 'NONE', #13468, 20.00000000000000355 ) ;
#5907=VERTEX_POINT ( 'NONE', #9821 ) ;
#5910=ORIENTED_EDGE ( 'NONE', *, *, #12663, .T. ) ;
#5931=EDGE_LOOP ( 'NONE', ( #20762, #6890, #17178, #20655 ) ) ;
#5938=VECTOR ( 'NONE', #4722, 1000.000000000000000 ) ;
#5949=ORIENTED_EDGE ( 'NONE', *, *, #16507, .F. ) ;
#5979=AXIS2_PLACEMENT_3D ( 'NONE', #19567, #1517, #11566 ) ;
#5996=CARTESIAN_POINT ( 'NONE',  ( -20.54277306141298354, 600.7448905601785327, -49.33244044267773631 ) ) ;
#5997=CARTESIAN_POINT ( 'NONE',  ( -28.68588794268875120, 610.7448905601785327, 0.000000000000000000 ) ) ;
#6036=CARTESIAN_POINT ( 'NONE',  ( 32.47532367400570052, 600.7448905601785327, 163.9643442751439011 ) ) ;
#6041=EDGE_LOOP ( 'NONE', ( #15712, #9599, #287, #11628 ) ) ;
#6090=EDGE_LOOP ( 'NONE', ( #12126, #2830, #7840, #1745 ) ) ;
#6095=CYLINDRICAL_SURFACE ( 'NONE', #11652, 200.0000000000000000 ) ;
#6097=DIRECTION ( 'NONE',  ( 1.000000000000000000, 0.000000000000000000, 0.000000000000000000 ) ) ;
#6118=VERTEX_POINT ( 'NONE', #18405 ) ;
#6128=CARTESIAN_POINT ( 'NONE',  ( -174.5421710038924346, 600.7448905601785327, -96.70028278950395872 ) ) ;
#6155=CIRCLE ( 'NONE', #4438, 175.0000000000000284 ) ;
#6162=VERTEX_POINT ( 'NONE', #18088 ) ;
#6163=PLANE ( 'NONE',  #3540 ) ;
#6182=CARTESIAN_POINT ( 'NONE',  ( -64.27068722059111394, 600.7448905601785327, 35.12437985717896538 ) ) ;
#6191=ORIENTED_EDGE ( 'NONE', *, *, #14386, .F. ) ;
#6192=LINE ( 'NONE', #16164, #5652 ) ;
#6203=DIRECTION ( 'NONE',  ( -1.191790137725560488E-16, 1.000000000000000000, 0.000000000000000000 ) ) ;
#6206=CARTESIAN_POINT ( 'NONE',  ( 171.3141120573112630, 610.7448905601785327, 0.000000000000000000 ) ) ;
#6213=VERTEX_POINT ( 'NONE', #11602 ) ;
#6223=VERTEX_POINT ( 'NONE', #11707 ) ;
#6241=CIRCLE ( 'NONE', #6592, 175.0000000000000284 ) ;
#6243=AXIS2_PLACEMENT_3D ( 'NONE', #11238, #19465, #4545 ) ;
#6271=CARTESIAN_POINT ( 'NONE',  ( -28.68588794268873698, 548.2448905601784190, 0.000000000000000000 ) ) ;
#6275=AXIS2_PLACEMENT_3D ( 'NONE', #9796, #14378, #16205 ) ;
#6286=CARTESIAN_POINT ( 'NONE',  ( 20.74841189052421697, 600.7448905601785327, -7.500000000000000000 ) ) ;
#6294=ORIENTED_EDGE ( 'NONE', *, *, #14622, .T. ) ;
#6317=CARTESIAN_POINT ( 'NONE',  ( 158.8141120573112630, 610.7448905601785327, 0.000000000000000000 ) ) ;
#6322=ORIENTED_EDGE ( 'NONE', *, *, #11218, .T. ) ;
#6333=ORIENTED_EDGE ( 'NONE', *, *, #3620, .T. ) ;
#6365=CARTESIAN_POINT ( 'NONE',  ( -28.68588794268874054, 588.2448905601785327, 0.000000000000000000 ) ) ;
#6378=EDGE_CURVE ( 'NONE', #7175, #10958, #14293, .T. ) ;
#6437=DIRECTION ( 'NONE',  ( -1.000000000000000000, 0.000000000000000000, 0.000000000000000000 ) ) ;
#6448=DIRECTION ( 'NONE',  ( 0.000000000000000000, 0.000000000000000000, 1.000000000000000000 ) ) ;
#6457=CARTESIAN_POINT ( 'NONE',  ( 158.8141120573112630, 575.7448905601785327, -10.00000000000000888 ) ) ;
#6477=VERTEX_POINT ( 'NONE', #11890 ) ;
#6510=ADVANCED_FACE ( 'NONE', ( #10468, #16985, #7011 ), #547, .F. ) ;
#6540=ORIENTED_EDGE ( 'NONE', *, *, #17426, .T. ) ;
#6565=ORIENTED_EDGE ( 'NONE', *, *, #1478, .F. ) ;
#6580=CARTESIAN_POINT ( 'NONE',  ( -28.68588794268875475, 600.7448905601785327, 0.000000000000000000 ) ) ;
#6583=EDGE_LOOP ( 'NONE', ( #10578, #13204 ) ) ;
#6592=AXIS2_PLACEMENT_3D ( 'NONE', #622, #9028, #7082 ) ;
#6630=CIRCLE ( 'NONE', #20459, 175.0000000000000284 ) ;
#6641=ORIENTED_EDGE ( 'NONE', *, *, #4197, .F. ) ;
#6652=ADVANCED_FACE ( 'NONE', ( #872 ), #15686, .F. ) ;
#6677=VERTEX_POINT ( 'NONE', #18800 ) ;
#6723=ORIENTED_EDGE ( 'NONE', *, *, #17374, .T. ) ;
#6736=CARTESIAN_POINT ( 'NONE',  ( -6.276925316985672687, 600.7448905601785327, -44.69718552705352721 ) ) ;
#6774=EDGE_CURVE ( 'NONE', #11578, #9304, #18758, .T. ) ;
#6825=EDGE_CURVE ( 'NONE', #445, #8097, #1393, .T. ) ;
#6881=EDGE_LOOP ( 'NONE', ( #10630, #2759, #6885, #17090 ) ) ;
#6884=CIRCLE ( 'NONE', #9646, 15.00000000000000355 ) ;
#6885=ORIENTED_EDGE ( 'NONE', *, *, #15192, .F. ) ;
#6890=ORIENTED_EDGE ( 'NONE', *, *, #14397, .T. ) ;
#6901=DIRECTION ( 'NONE',  ( 0.000000000000000000, 0.000000000000000000, 1.000000000000000000 ) ) ;
#6926=DIRECTION ( 'NONE',  ( -0.3090169943749472292, 0.000000000000000000, 0.9510565162951536422 ) ) ;
#6930=ORIENTED_EDGE ( 'NONE', *, *, #16959, .F. ) ;
#6933=VERTEX_POINT ( 'NONE', #21281 ) ;
#6937=ORIENTED_EDGE ( 'NONE', *, *, #6825, .T. ) ;
#7011=FACE_OUTER_BOUND ( 'NONE', #2271, .T. ) ;
#7031=FACE_OUTER_BOUND ( 'NONE', #2777, .T. ) ;
#7042=DIRECTION ( 'NONE',  ( 0.3090169943749472847, -0.000000000000000000, -0.9510565162951536422 ) ) ;
#7082=DIRECTION ( 'NONE',  ( 0.000000000000000000, 0.000000000000000000, 1.000000000000000000 ) ) ;
#7088=EDGE_CURVE ( 'NONE', #15582, #445, #20595, .T. ) ;
#7090=FACE_OUTER_BOUND ( 'NONE', #708, .T. ) ;
#7095=ORIENTED_EDGE ( 'NONE', *, *, #6825, .F. ) ;
#7115=CIRCLE ( 'NONE', #3341, 200.0000000000000000 ) ;
#7134=DIRECTION ( 'NONE',  ( 1.191790137725560488E-16, -1.000000000000000000, -0.000000000000000000 ) ) ;
#7159=DIRECTION ( 'NONE',  ( 0.000000000000000000, 0.000000000000000000, 1.000000000000000000 ) ) ;
#7166=EDGE_CURVE ( 'NONE', #6213, #8588, #14306, .T. ) ;
#7172=CARTESIAN_POINT ( 'NONE',  ( -174.5421710038924061, 600.7448905601785327, 96.70028278950401557 ) ) ;
#7175=VERTEX_POINT ( 'NONE', #9119 ) ;
#7182=DIRECTION ( 'NONE',  ( 0.000000000000000000, 0.000000000000000000, 1.000000000000000000 ) ) ;
#7228=PRODUCT_DEFINITION ( 'UNKNOWN', '', #10726, #17212 ) ;
#7239=PLANE ( 'NONE',  #2179 ) ;
#7250=LINE ( 'NONE', #476, #9472 ) ;
#7307=EDGE_CURVE ( 'NONE', #9225, #11682, #6192, .T. ) ;
#7353=ADVANCED_FACE ( 'NONE', ( #7090 ), #3437, .T. ) ;
#7357=ORIENTED_EDGE ( 'NONE', *, *, #210, .T. ) ;
#7390=CARTESIAN_POINT ( 'NONE',  ( -165.7253922195053519, 585.7448905601785327, -108.8355377051282034 ) ) ;
#7404=CARTESIAN_POINT ( 'NONE',  ( -28.68588794268874054, 588.2448905601785327, 0.000000000000000000 ) ) ;
#7412=EDGE_LOOP ( 'NONE', ( #6565, #1806, #8606, #18909 ) ) ;
#7418=ORIENTED_EDGE ( 'NONE', *, *, #14268, .T. ) ;
#7425=LINE ( 'NONE', #5598, #775 ) ;
#7468=DIRECTION ( 'NONE',  ( 0.000000000000000000, 0.000000000000000000, 1.000000000000000000 ) ) ;
#7507=DIRECTION ( 'NONE',  ( 0.000000000000000000, 0.000000000000000000, 1.000000000000000000 ) ) ;
#7509=DIRECTION ( 'NONE',  ( 0.000000000000000000, 1.000000000000000000, -0.000000000000000000 ) ) ;
#7518=ORIENTED_EDGE ( 'NONE', *, *, #3500, .F. ) ;
#7568=ORIENTED_EDGE ( 'NONE', *, *, #2723, .F. ) ;
#7588=DIRECTION ( 'NONE',  ( 1.191790137725560488E-16, -1.000000000000000000, -0.000000000000000000 ) ) ;
#7609=FACE_OUTER_BOUND ( 'NONE', #3251, .T. ) ;
#7612=VECTOR ( 'NONE', #12054, 1000.000000000000114 ) ;
#7685=ADVANCED_FACE ( 'NONE', ( #17896 ), #16297, .T. ) ;
#7694=CARTESIAN_POINT ( 'NONE',  ( 8.938426032941704028E-16, 585.7448905601785327, 0.000000000000000000 ) ) ;
#7722=LINE ( 'NONE', #17992, #10099 ) ;
#7724=DIRECTION ( 'NONE',  ( 0.000000000000000000, 0.000000000000000000, 1.000000000000000000 ) ) ;
#7772=DIRECTION ( 'NONE',  ( 0.000000000000000000, 1.000000000000000000, -0.000000000000000000 ) ) ;
#7822=DIRECTION ( 'NONE',  ( -1.000000000000000000, 0.000000000000000000, 0.000000000000000000 ) ) ;
#7825=AXIS2_PLACEMENT_3D ( 'NONE', #11296, #9464, #16076 ) ;
#7836=DIRECTION ( 'NONE',  ( 0.000000000000000000, 1.000000000000000000, 0.000000000000000000 ) ) ;
#7840=ORIENTED_EDGE ( 'NONE', *, *, #4197, .T. ) ;
#7878=DIRECTION ( 'NONE',  ( 0.000000000000000000, 0.000000000000000000, 1.000000000000000000 ) ) ;
#7883=ORIENTED_EDGE ( 'NONE', *, *, #10215, .T. ) ;
#7918=EDGE_LOOP ( 'NONE', ( #4612, #11403, #3595, #18505 ) ) ;
#7953=DIRECTION ( 'NONE',  ( 0.000000000000000000, 0.000000000000000000, 1.000000000000000000 ) ) ;
#7989=VERTEX_POINT ( 'NONE', #2150 ) ;
#8010=EDGE_CURVE ( 'NONE', #20333, #2560, #20531, .T. ) ;
#8050=AXIS2_PLACEMENT_3D ( 'NONE', #16559, #10254, #18162 ) ;
#8054=CIRCLE ( 'NONE', #17732, 175.0000000000000284 ) ;
#8060=LINE ( 'NONE', #9792, #19597 ) ;
#8097=VERTEX_POINT ( 'NONE', #19118 ) ;
#8139=DIRECTION ( 'NONE',  ( 0.000000000000000000, 0.000000000000000000, 1.000000000000000000 ) ) ;
#8145=EDGE_CURVE ( 'NONE', #11996, #445, #6155, .T. ) ;
#8159=DIRECTION ( 'NONE',  ( 1.191790137725560488E-16, -1.000000000000000000, -0.000000000000000000 ) ) ;
#8160=VECTOR ( 'NONE', #8580, 1000.000000000000000 ) ;
#8194=ADVANCED_FACE ( 'NONE', ( #11100 ), #16091, .T. ) ;
#8196=AXIS2_PLACEMENT_3D ( 'NONE', #6365, #12974, #19565 ) ;
#8212=CARTESIAN_POINT ( 'NONE',  ( -43.68588794268873698, 548.2448905601784190, 1.836970198721029194E-15 ) ) ;
#8234=ORIENTED_EDGE ( 'NONE', *, *, #13735, .T. ) ;
#8244=EDGE_CURVE ( 'NONE', #7989, #9304, #16310, .T. ) ;
#8315=ORIENTED_EDGE ( 'NONE', *, *, #8145, .T. ) ;
#8317=ORIENTED_EDGE ( 'NONE', *, *, #18289, .F. ) ;
#8324=ORIENTED_EDGE ( 'NONE', *, *, #16321, .F. ) ;
#8329=CYLINDRICAL_SURFACE ( 'NONE', #14166, 50.00000000000000000 ) ;
#8344=EDGE_CURVE ( 'NONE', #14887, #19850, #10306, .T. ) ;
#8414=CARTESIAN_POINT ( 'NONE',  ( -6.276925316985663805, 600.7448905601785327, 44.69718552705352010 ) ) ;
#8423=VERTEX_POINT ( 'NONE', #13915 ) ;
#8434=VECTOR ( 'NONE', #12912, 1000.000000000000000 ) ;
#8488=ORIENTED_EDGE ( 'NONE', *, *, #16321, .T. ) ;
#8507=ADVANCED_FACE ( 'NONE', ( #3841 ), #5352, .F. ) ;
#8533=ORIENTED_EDGE ( 'NONE', *, *, #14991, .T. ) ;
#8544=CARTESIAN_POINT ( 'NONE',  ( 20.74841189052421697, 600.7448905601785327, 7.500000000000000000 ) ) ;
#8561=CARTESIAN_POINT ( 'NONE',  ( 146.1533239063698772, 600.7448905601785327, -7.500000000000000000 ) ) ;
#8580=DIRECTION ( 'NONE',  ( 1.191790137725560488E-16, -1.000000000000000000, -0.000000000000000000 ) ) ;
#8584=ORIENTED_EDGE ( 'NONE', *, *, #15971, .F. ) ;
#8588=VERTEX_POINT ( 'NONE', #20289 ) ;
#8606=ORIENTED_EDGE ( 'NONE', *, *, #21219, .T. ) ;
#8618=AXIS2_PLACEMENT_3D ( 'NONE', #12714, #11291, #14244 ) ;
#8651=AXIS2_PLACEMENT_3D ( 'NONE', #15827, #9921, #2620 ) ;
#8700=LINE ( 'NONE', #15322, #7612 ) ;
#8711=LINE ( 'NONE', #2130, #9700 ) ;
#8726=CIRCLE ( 'NONE', #5271, 20.00000000000000355 ) ;
#8740=DIRECTION ( 'NONE',  ( 0.000000000000000000, 1.000000000000000000, -0.000000000000000000 ) ) ;
#8743=EDGE_CURVE ( 'NONE', #21019, #7175, #15750, .T. ) ;
#8756=EDGE_CURVE ( 'NONE', #11085, #4497, #11710, .T. ) ;
#8768=CARTESIAN_POINT ( 'NONE',  ( -228.6858879426887654, 610.7448905601785327, 2.449293598294706434E-14 ) ) ;
#8866=AXIS2_PLACEMENT_3D ( 'NONE', #5232, #18738, #7159 ) ;
#8873=ORIENTED_EDGE ( 'NONE', *, *, #14673, .F. ) ;
#8907=CARTESIAN_POINT ( 'NONE',  ( -28.68588794268875120, 610.7448905601785327, 0.000000000000000000 ) ) ;
#8917=CARTESIAN_POINT ( 'NONE',  ( 8.938426032941704028E-16, 585.7448905601785327, 7.500000000000000000 ) ) ;
#8919=DIRECTION ( 'NONE',  ( 0.000000000000000000, 1.000000000000000000, -0.000000000000000000 ) ) ;
#8990=AXIS2_PLACEMENT_3D ( 'NONE', #9576, #9891, #21261 ) ;
#9012=ORIENTED_EDGE ( 'NONE', *, *, #18289, .T. ) ;
#9028=DIRECTION ( 'NONE',  ( 0.000000000000000000, 1.000000000000000000, -0.000000000000000000 ) ) ;
#9080=VECTOR ( 'NONE', #21090, 1000.000000000000114 ) ;
#9104=LINE ( 'NONE', #4131, #17922 ) ;
#9113=CARTESIAN_POINT ( 'NONE',  ( -8.938426032941704028E-16, 600.7448905601785327, 0.000000000000000000 ) ) ;
#9118=ORIENTED_EDGE ( 'NONE', *, *, #4262, .T. ) ;
#9119=CARTESIAN_POINT ( 'NONE',  ( -20.54277306141297998, 585.7448905601785327, -49.33244044267773631 ) ) ;
#9131=CARTESIAN_POINT ( 'NONE',  ( -28.68588794268873698, 548.2448905601784190, 0.000000000000000000 ) ) ;
#9214=LINE ( 'NONE', #4461, #14080 ) ;
#9223=EDGE_CURVE ( 'NONE', #11679, #12774, #9104, .T. ) ;
#9225=VERTEX_POINT ( 'NONE', #19275 ) ;
#9229=DIRECTION ( 'NONE',  ( 0.000000000000000000, 0.000000000000000000, 1.000000000000000000 ) ) ;
#9258=ORIENTED_EDGE ( 'NONE', *, *, #17558, .T. ) ;
#9268=CARTESIAN_POINT ( 'NONE',  ( 158.8141120573112630, 10.52886280891152104, -10.00000000000000888 ) ) ;
#9286=EDGE_LOOP ( 'NONE', ( #17430, #9515, #2404, #3390 ) ) ;
#9288=ORIENTED_EDGE ( 'NONE', *, *, #3168, .F. ) ;
#9304=VERTEX_POINT ( 'NONE', #1123 ) ;
#9306=CARTESIAN_POINT ( 'NONE',  ( -28.68588794268875120, 585.7448905601785327, 0.000000000000000000 ) ) ;
#9321=CARTESIAN_POINT ( 'NONE',  ( -28.68588794268874409, 608.2448905601786464, 0.000000000000000000 ) ) ;
#9340=ADVANCED_FACE ( 'NONE', ( #12469, #4352 ), #10936, .F. ) ;
#9344=CARTESIAN_POINT ( 'NONE',  ( -28.68588794268873698, 548.2448905601784190, 0.000000000000000000 ) ) ;
#9351=VECTOR ( 'NONE', #7588, 1000.000000000000000 ) ;
#9352=CYLINDRICAL_SURFACE ( 'NONE', #1813, 20.00000000000000355 ) ;
#9376=CARTESIAN_POINT ( 'NONE',  ( -28.68588794268875475, 600.7448905601785327, 0.000000000000000000 ) ) ;
#9391=ORIENTED_EDGE ( 'NONE', *, *, #4262, .F. ) ;
#9407=EDGE_CURVE ( 'NONE', #11603, #827, #5852, .T. ) ;
#9412=ORIENTED_EDGE ( 'NONE', *, *, #8010, .T. ) ;
#9442=ORIENTED_EDGE ( 'NONE', *, *, #15987, .F. ) ;
#9460=DIRECTION ( 'NONE',  ( 0.000000000000000000, 0.000000000000000000, 1.000000000000000000 ) ) ;
#9464=DIRECTION ( 'NONE',  ( 0.5877852522924732481, 7.005166667826999217E-17, 0.8090169943749473402 ) ) ;
#9472=VECTOR ( 'NONE', #7042, 1000.000000000000000 ) ;
#9496=ORIENTED_EDGE ( 'NONE', *, *, #4719, .F. ) ;
#9511=DIRECTION ( 'NONE',  ( 0.9510565162951535312, 1.133459776540192417E-16, -0.3090169943749475068 ) ) ;
#9515=ORIENTED_EDGE ( 'NONE', *, *, #9407, .T. ) ;
#9516=VERTEX_POINT ( 'NONE', #4878 ) ;
#9529=( NAMED_UNIT ( * ) SI_UNIT ( $, .STERADIAN. ) SOLID_ANGLE_UNIT ( ) );
#9543=LINE ( 'NONE', #1448, #8434 ) ;
#9555=DIRECTION ( 'NONE',  ( 0.000000000000000000, 1.000000000000000000, -0.000000000000000000 ) ) ;
#9565=PLANE ( 'NONE',  #7825 ) ;
#9576=CARTESIAN_POINT ( 'NONE',  ( -8.938426032941704028E-16, 600.7448905601785327, -7.500000000000000000 ) ) ;
#9589=FACE_OUTER_BOUND ( 'NONE', #14289, .T. ) ;
#9599=ORIENTED_EDGE ( 'NONE', *, *, #9223, .T. ) ;
#9632=AXIS2_PLACEMENT_3D ( 'NONE', #5674, #10217, #5568 ) ;
#9646=AXIS2_PLACEMENT_3D ( 'NONE', #13081, #16227, #19459 ) ;
#9686=AXIS2_PLACEMENT_3D ( 'NONE', #1306, #890, #14301 ) ;
#9687=CARTESIAN_POINT ( 'NONE',  ( -28.68588794268873698, 548.2448905601784190, 0.000000000000000000 ) ) ;
#9690=CIRCLE ( 'NONE', #16272, 50.00000000000000000 ) ;
#9700=VECTOR ( 'NONE', #2658, 1000.000000000000000 ) ;
#9716=AXIS2_PLACEMENT_3D ( 'NONE', #17952, #3149, #9730 ) ;
#9730=DIRECTION ( 'NONE',  ( 1.000000000000000000, 0.000000000000000000, 0.000000000000000000 ) ) ;
#9769=FACE_OUTER_BOUND ( 'NONE', #120, .T. ) ;
#9776=ORIENTED_EDGE ( 'NONE', *, *, #17031, .T. ) ;
#9777=CARTESIAN_POINT ( 'NONE',  ( -28.68588794268874409, 608.2448905601786464, 0.000000000000000000 ) ) ;
#9792=CARTESIAN_POINT ( 'NONE',  ( -165.7253922195052951, 600.7448905601785327, 108.8355377051282176 ) ) ;
#9794=FACE_OUTER_BOUND ( 'NONE', #14336, .T. ) ;
#9796=CARTESIAN_POINT ( 'NONE',  ( -28.68588794268874054, 588.2448905601785327, 0.000000000000000000 ) ) ;
#9821=CARTESIAN_POINT ( 'NONE',  ( -174.5421710038924061, 585.7448905601785327, -96.70028278950395872 ) ) ;
#9822=DIRECTION ( 'NONE',  ( 0.000000000000000000, 1.000000000000000000, -0.000000000000000000 ) ) ;
#9825=VERTEX_POINT ( 'NONE', #8544 ) ;
#9856=ORIENTED_EDGE ( 'NONE', *, *, #8756, .F. ) ;
#9859=ADVANCED_FACE ( 'NONE', ( #17102 ), #8329, .T. ) ;
#9862=DIRECTION ( 'NONE',  ( 0.000000000000000000, 0.000000000000000000, 1.000000000000000000 ) ) ;
#9876=EDGE_CURVE ( 'NONE', #13766, #6118, #15907, .T. ) ;
#9891=DIRECTION ( 'NONE',  ( 0.000000000000000000, 0.000000000000000000, -1.000000000000000000 ) ) ;
#9921=DIRECTION ( 'NONE',  ( 0.000000000000000000, 1.000000000000000000, -0.000000000000000000 ) ) ;
#9940=ORIENTED_EDGE ( 'NONE', *, *, #5202, .F. ) ;
#9961=CARTESIAN_POINT ( 'NONE',  ( -28.68588794268875120, 610.7448905601785327, 0.000000000000000000 ) ) ;
#9973=DIRECTION ( 'NONE',  ( 0.000000000000000000, 0.000000000000000000, 1.000000000000000000 ) ) ;
#10014=EDGE_CURVE ( 'NONE', #10551, #17415, #6884, .T. ) ;
#10024=EDGE_LOOP ( 'NONE', ( #3648, #1661, #9012, #17944 ) ) ;
#10094=CARTESIAN_POINT ( 'NONE',  ( -6.276925316985663805, 600.7448905601785327, 44.69718552705352010 ) ) ;
#10098=LINE ( 'NONE', #19955, #8160 ) ;
#10099=VECTOR ( 'NONE', #11074, 1000.000000000000000 ) ;
#10162=VECTOR ( 'NONE', #20354, 1000.000000000000000 ) ;
#10184=CARTESIAN_POINT ( 'NONE',  ( 32.47532367400570052, 600.7448905601785327, 163.9643442751439011 ) ) ;
#10190=DIRECTION ( 'NONE',  ( 1.191790137725560488E-16, -1.000000000000000000, -0.000000000000000000 ) ) ;
#10195=CARTESIAN_POINT ( 'NONE',  ( -13.68588794268874054, 588.2448905601785327, 0.000000000000000000 ) ) ;
#10215=EDGE_CURVE ( 'NONE', #12217, #1162, #19667, .T. ) ;
#10217=DIRECTION ( 'NONE',  ( -0.9510565162951537532, -1.133459776540192910E-16, -0.3090169943749470627 ) ) ;
#10225=AXIS2_PLACEMENT_3D ( 'NONE', #5100, #16366, #18184 ) ;
#10239=AXIS2_PLACEMENT_3D ( 'NONE', #16499, #19949, #1796 ) ;
#10254=DIRECTION ( 'NONE',  ( 0.000000000000000000, 1.000000000000000000, -0.000000000000000000 ) ) ;
#10306=CIRCLE ( 'NONE', #12031, 20.00000000000000711 ) ;
#10329=FACE_OUTER_BOUND ( 'NONE', #19573, .T. ) ;
#10377=CIRCLE ( 'NONE', #1086, 200.0000000000000000 ) ;
#10390=CIRCLE ( 'NONE', #8618, 10.00000000000000888 ) ;
#10396=LINE ( 'NONE', #20574, #45 ) ;
#10415=VERTEX_POINT ( 'NONE', #10632 ) ;
#10436=AXIS2_PLACEMENT_3D ( 'NONE', #9131, #18652, #12284 ) ;
#10447=ORIENTED_EDGE ( 'NONE', *, *, #4778, .F. ) ;
#10468=FACE_BOUND ( 'NONE', #5054, .T. ) ;
#10469=EDGE_LOOP ( 'NONE', ( #20940, #6930, #4142, #5693 ) ) ;
#10512=LINE ( 'NONE', #17135, #15122 ) ;
#10513=LINE ( 'NONE', #10728, #14220 ) ;
#10531=ADVANCED_FACE ( 'NONE', ( #1748, #1638, #129 ), #13099, .T. ) ;
#10551=VERTEX_POINT ( 'NONE', #8212 ) ;
#10578=ORIENTED_EDGE ( 'NONE', *, *, #15983, .F. ) ;
#10601=ORIENTED_EDGE ( 'NONE', *, *, #17374, .F. ) ;
#10630=ORIENTED_EDGE ( 'NONE', *, *, #6378, .T. ) ;
#10632=CARTESIAN_POINT ( 'NONE',  ( -64.27068722059111394, 600.7448905601785327, 35.12437985717896538 ) ) ;
#10639=DIRECTION ( 'NONE',  ( 1.191790137725560488E-16, -1.000000000000000000, -0.000000000000000000 ) ) ;
#10682=ORIENTED_EDGE ( 'NONE', *, *, #12490, .F. ) ;
#10685=VERTEX_POINT ( 'NONE', #11249 ) ;
#10713=ADVANCED_FACE ( 'NONE', ( #4759 ), #11355, .T. ) ;
#10726=PRODUCT_DEFINITION_FORMATION_WITH_SPECIFIED_SOURCE ( 'ANY', '', #5764, .NOT_KNOWN. ) ;
#10728=CARTESIAN_POINT ( 'NONE',  ( -14.31911992702480063, 585.7448905601785327, 19.70857778461545351 ) ) ;
#10740=DIRECTION ( 'NONE',  ( 0.000000000000000000, 1.000000000000000000, -0.000000000000000000 ) ) ;
#10775=DIRECTION ( 'NONE',  ( 1.000000000000000000, 0.000000000000000000, 0.000000000000000000 ) ) ;
#10792=DIRECTION ( 'NONE',  ( -1.191790137725560488E-16, 1.000000000000000000, 0.000000000000000000 ) ) ;
#10805=CARTESIAN_POINT ( 'NONE',  ( -18.81370552131602381, 585.7448905601785327, -6.112943483001347822 ) ) ;
#10820=ORIENTED_EDGE ( 'NONE', *, *, #577, .F. ) ;
#10863=CARTESIAN_POINT ( 'NONE',  ( 158.8141120573112630, 610.7448905601785327, 0.000000000000000000 ) ) ;
#10882=DIRECTION ( 'NONE',  ( 0.5877852522924733591, 7.005166667827000450E-17, 0.8090169943749473402 ) ) ;
#10905=ORIENTED_EDGE ( 'NONE', *, *, #15971, .T. ) ;
#10936=PLANE ( 'NONE',  #15521 ) ;
#10941=CARTESIAN_POINT ( 'NONE',  ( -73.08746600497821078, 585.7448905601785327, 22.98912494155475628 ) ) ;
#10958=VERTEX_POINT ( 'NONE', #15901 ) ;
#10993=VECTOR ( 'NONE', #18785, 1000.000000000000000 ) ;
#11003=VECTOR ( 'NONE', #20826, 1000.000000000000000 ) ;
#11011=ORIENTED_EDGE ( 'NONE', *, *, #15553, .F. ) ;
#11052=ORIENTED_EDGE ( 'NONE', *, *, #492, .T. ) ;
#11053=VECTOR ( 'NONE', #744, 1000.000000000000114 ) ;
#11062=DIRECTION ( 'NONE',  ( 0.000000000000000000, 1.000000000000000000, -0.000000000000000000 ) ) ;
#11072=DIRECTION ( 'NONE',  ( 0.000000000000000000, 1.000000000000000000, -0.000000000000000000 ) ) ;
#11074=DIRECTION ( 'NONE',  ( 1.191790137725560488E-16, -1.000000000000000000, -0.000000000000000000 ) ) ;
#11085=VERTEX_POINT ( 'NONE', #3123 ) ;
#11088=ORIENTED_EDGE ( 'NONE', *, *, #14673, .T. ) ;
#11100=FACE_OUTER_BOUND ( 'NONE', #6881, .T. ) ;
#11116=ORIENTED_EDGE ( 'NONE', *, *, #18647, .F. ) ;
#11123=AXIS2_PLACEMENT_3D ( 'NONE', #15434, #518, #12504 ) ;
#11129=LINE ( 'NONE', #1407, #20984 ) ;
#11158=DIRECTION ( 'NONE',  ( 0.000000000000000000, 0.000000000000000000, -1.000000000000000000 ) ) ;
#11187=DIRECTION ( 'NONE',  ( 1.191790137725560488E-16, -1.000000000000000000, -0.000000000000000000 ) ) ;
#11194=VERTEX_POINT ( 'NONE', #6457 ) ;
#11218=EDGE_CURVE ( 'NONE', #20333, #11194, #17677, .T. ) ;
#11238=CARTESIAN_POINT ( 'NONE',  ( -28.68588794268875475, 600.7448905601785327, 0.000000000000000000 ) ) ;
#11241=CARTESIAN_POINT ( 'NONE',  ( -14.31911992702480951, 600.7448905601785327, -19.70857778461545351 ) ) ;
#11246=ORIENTED_EDGE ( 'NONE', *, *, #18469, .F. ) ;
#11249=CARTESIAN_POINT ( 'NONE',  ( -64.27068722059111394, 585.7448905601785327, 35.12437985717896538 ) ) ;
#11271=EDGE_LOOP ( 'NONE', ( #1417, #12160, #17175, #11088 ) ) ;
#11291=DIRECTION ( 'NONE',  ( 0.000000000000000000, 1.000000000000000000, -0.000000000000000000 ) ) ;
#11296=CARTESIAN_POINT ( 'NONE',  ( -14.31911992702480951, 600.7448905601785327, -19.70857778461545351 ) ) ;
#11310=CIRCLE ( 'NONE', #8196, 15.00000000000000000 ) ;
#11315=CARTESIAN_POINT ( 'NONE',  ( -203.6858879426887654, 610.7448905601785327, 2.143131898507868248E-14 ) ) ;
#11350=EDGE_LOOP ( 'NONE', ( #20521, #6191, #17615, #13538 ) ) ;
#11355=CYLINDRICAL_SURFACE ( 'NONE', #9716, 20.00000000000000355 ) ;
#11361=AXIS2_PLACEMENT_3D ( 'NONE', #17259, #832, #14451 ) ;
#11370=CARTESIAN_POINT ( 'NONE',  ( 8.938426032941704028E-16, 585.7448905601785327, -7.500000000000000000 ) ) ;
#11391=CARTESIAN_POINT ( 'NONE',  ( -20.54277306141298354, 600.7448905601785327, -49.33244044267773631 ) ) ;
#11393=DIRECTION ( 'NONE',  ( 1.191790137725560488E-16, -1.000000000000000000, -0.000000000000000000 ) ) ;
#11403=ORIENTED_EDGE ( 'NONE', *, *, #210, .F. ) ;
#11431=VECTOR ( 'NONE', #18211, 1000.000000000000000 ) ;
#11439=ORIENTED_EDGE ( 'NONE', *, *, #6774, .F. ) ;
#11460=ORIENTED_EDGE ( 'NONE', *, *, #7088, .F. ) ;
#11471=EDGE_CURVE ( 'NONE', #10685, #15951, #15559, .T. ) ;
#11483=EDGE_CURVE ( 'NONE', #10958, #289, #18780, .T. ) ;
#11491=ORIENTED_EDGE ( 'NONE', *, *, #9876, .F. ) ;
#11505=DIRECTION ( 'NONE',  ( 1.191790137725560488E-16, -1.000000000000000000, -0.000000000000000000 ) ) ;
#11566=DIRECTION ( 'NONE',  ( 1.000000000000000000, 0.000000000000000000, 0.000000000000000000 ) ) ;
#11569=ORIENTED_EDGE ( 'NONE', *, *, #6378, .F. ) ;
#11571=ORIENTED_EDGE ( 'NONE', *, *, #16439, .T. ) ;
#11578=VERTEX_POINT ( 'NONE', #18997 ) ;
#11590=DIRECTION ( 'NONE',  ( -0.5877852522924731371, -7.005166667826997985E-17, 0.8090169943749475623 ) ) ;
#11591=UNCERTAINTY_MEASURE_WITH_UNIT (LENGTH_MEASURE( 1.000000000000000082E-05 ), #14527, 'distance_accuracy_value', 'NONE');
#11597=ORIENTED_EDGE ( 'NONE', *, *, #15273, .T. ) ;
#11602=CARTESIAN_POINT ( 'NONE',  ( 171.3141120573112630, 610.7448905601785327, 0.000000000000000000 ) ) ;
#11603=VERTEX_POINT ( 'NONE', #1585 ) ;
#11617=PLANE ( 'NONE',  #10239 ) ;
#11628=ORIENTED_EDGE ( 'NONE', *, *, #3009, .F. ) ;
#11652=AXIS2_PLACEMENT_3D ( 'NONE', #5997, #17785, #12710 ) ;
#11667=DIRECTION ( 'NONE',  ( 1.191790137725560488E-16, -1.000000000000000000, -0.000000000000000000 ) ) ;
#11669=LINE ( 'NONE', #20608, #2689 ) ;
#11674=ADVANCED_FACE ( 'NONE', ( #18116 ), #14470, .T. ) ;
#11679=VERTEX_POINT ( 'NONE', #16514 ) ;
#11682=VERTEX_POINT ( 'NONE', #20947 ) ;
#11685=CARTESIAN_POINT ( 'NONE',  ( -2.085632741019731137E-15, 610.7448905601785327, 0.000000000000000000 ) ) ;
#11698=DIRECTION ( 'NONE',  ( 0.000000000000000000, 0.000000000000000000, -1.000000000000000000 ) ) ;
#11707=CARTESIAN_POINT ( 'NONE',  ( 18.20947592957834260, 600.7448905601785327, -168.5995991907681173 ) ) ;
#11710=CIRCLE ( 'NONE', #11361, 50.00000000000000000 ) ;
#11766=VERTEX_POINT ( 'NONE', #3628 ) ;
#11824=EDGE_CURVE ( 'NONE', #11085, #8097, #8700, .T. ) ;
#11827=DIRECTION ( 'NONE',  ( 1.191790137725560488E-16, -1.000000000000000000, -0.000000000000000000 ) ) ;
#11836=VECTOR ( 'NONE', #18553, 1000.000000000000000 ) ;
#11841=ORIENTED_EDGE ( 'NONE', *, *, #14991, .F. ) ;
#11886=FACE_OUTER_BOUND ( 'NONE', #14092, .T. ) ;
#11890=CARTESIAN_POINT ( 'NONE',  ( 146.1533239063698772, 600.7448905601785327, -7.500000000000000000 ) ) ;
#11970=AXIS2_PLACEMENT_3D ( 'NONE', #18956, #12042, #17242 ) ;
#11996=VERTEX_POINT ( 'NONE', #3180 ) ;
#12031=AXIS2_PLACEMENT_3D ( 'NONE', #9687, #18123, #6437 ) ;
#12042=DIRECTION ( 'NONE',  ( 0.000000000000000000, 1.000000000000000000, -0.000000000000000000 ) ) ;
#12054=DIRECTION ( 'NONE',  ( 0.3090169943749475068, 0.000000000000000000, 0.9510565162951535312 ) ) ;
#12096=CARTESIAN_POINT ( 'NONE',  ( 146.1533239063698772, 585.7448905601785327, -7.500000000000000000 ) ) ;
#12100=CARTESIAN_POINT ( 'NONE',  ( -28.68588794268874054, 588.2448905601785327, 0.000000000000000000 ) ) ;
#12120=LINE ( 'NONE', #2075, #4745 ) ;
#12126=ORIENTED_EDGE ( 'NONE', *, *, #18225, .F. ) ;
#12135=EDGE_CURVE ( 'NONE', #6677, #11766, #12478, .T. ) ;
#12160=ORIENTED_EDGE ( 'NONE', *, *, #10215, .F. ) ;
#12206=AXIS2_PLACEMENT_3D ( 'NONE', #12100, #10792, #15262 ) ;
#12217=VERTEX_POINT ( 'NONE', #18619 ) ;
#12222=AXIS2_PLACEMENT_3D ( 'NONE', #16854, #15025, #13711 ) ;
#12245=EDGE_LOOP ( 'NONE', ( #981, #83, #13037, #13039 ) ) ;
#12246=DIRECTION ( 'NONE',  ( 0.000000000000000000, 0.000000000000000000, 1.000000000000000000 ) ) ;
#12284=DIRECTION ( 'NONE',  ( -1.000000000000000000, 0.000000000000000000, 0.000000000000000000 ) ) ;
#12365=CARTESIAN_POINT ( 'NONE',  ( -28.68588794268874764, 575.7448905601785327, 0.000000000000000000 ) ) ;
#12368=CARTESIAN_POINT ( 'NONE',  ( -165.7253922195053519, 600.7448905601785327, -108.8355377051282034 ) ) ;
#12405=CARTESIAN_POINT ( 'NONE',  ( -5.502341142637719784, 585.7448905601785327, -7.573322868991255952 ) ) ;
#12454=FACE_OUTER_BOUND ( 'NONE', #17478, .T. ) ;
#12461=CIRCLE ( 'NONE', #9686, 50.00000000000000000 ) ;
#12465=CIRCLE ( 'NONE', #8651, 175.0000000000000284 ) ;
#12469=FACE_OUTER_BOUND ( 'NONE', #15136, .T. ) ;
#12471=VECTOR ( 'NONE', #8159, 1000.000000000000000 ) ;
#12478=CIRCLE ( 'NONE', #1424, 175.0000000000000284 ) ;
#12490=EDGE_CURVE ( 'NONE', #8423, #15264, #19728, .T. ) ;
#12504=DIRECTION ( 'NONE',  ( 1.000000000000000000, 0.000000000000000000, 0.000000000000000000 ) ) ;
#12505=DIRECTION ( 'NONE',  ( 0.000000000000000000, 1.000000000000000000, -0.000000000000000000 ) ) ;
#12583=FACE_OUTER_BOUND ( 'NONE', #6041, .T. ) ;
#12595=EDGE_CURVE ( 'NONE', #9304, #11578, #6241, .T. ) ;
#12663=EDGE_CURVE ( 'NONE', #6223, #6933, #8711, .T. ) ;
#12669=ORIENTED_EDGE ( 'NONE', *, *, #18931, .T. ) ;
#12674=CIRCLE ( 'NONE', #1988, 50.00000000000000000 ) ;
#12710=DIRECTION ( 'NONE',  ( 1.000000000000000000, 0.000000000000000000, 0.000000000000000000 ) ) ;
#12714=CARTESIAN_POINT ( 'NONE',  ( 158.8141120573112630, 575.7448905601785327, 0.000000000000000000 ) ) ;
#12722=ORIENTED_EDGE ( 'NONE', *, *, #15553, .T. ) ;
#12753=EDGE_LOOP ( 'NONE', ( #1961, #18991, #16240, #8873 ) ) ;
#12757=EDGE_CURVE ( 'NONE', #15706, #2560, #16287, .T. ) ;
#12774=VERTEX_POINT ( 'NONE', #16073 ) ;
#12794=AXIS2_PLACEMENT_3D ( 'NONE', #808, #2419, #696 ) ;
#12801=EDGE_LOOP ( 'NONE', ( #20388, #1838 ) ) ;
#12835=ORIENTED_EDGE ( 'NONE', *, *, #522, .T. ) ;
#12859=ORIENTED_EDGE ( 'NONE', *, *, #5038, .T. ) ;
#12863=ORIENTED_EDGE ( 'NONE', *, *, #577, .T. ) ;
#12876=CIRCLE ( 'NONE', #13582, 20.00000000000000355 ) ;
#12912=DIRECTION ( 'NONE',  ( 0.3090169943749472847, -0.000000000000000000, -0.9510565162951536422 ) ) ;
#12962=VERTEX_POINT ( 'NONE', #20585 ) ;
#12974=DIRECTION ( 'NONE',  ( -1.191790137725560488E-16, 1.000000000000000000, 0.000000000000000000 ) ) ;
#13001=CYLINDRICAL_SURFACE ( 'NONE', #16158, 50.00000000000000000 ) ;
#13028=AXIS2_PLACEMENT_3D ( 'NONE', #9113, #15734, #18532 ) ;
#13037=ORIENTED_EDGE ( 'NONE', *, *, #14268, .F. ) ;
#13039=ORIENTED_EDGE ( 'NONE', *, *, #16657, .T. ) ;
#13046=ORIENTED_EDGE ( 'NONE', *, *, #16507, .T. ) ;
#13054=DIRECTION ( 'NONE',  ( 1.191790137725560488E-16, -1.000000000000000000, -0.000000000000000000 ) ) ;
#13081=CARTESIAN_POINT ( 'NONE',  ( -28.68588794268873698, 548.2448905601784190, 0.000000000000000000 ) ) ;
#13090=DIRECTION ( 'NONE',  ( -0.8090169943749473402, 0.000000000000000000, 0.5877852522924732481 ) ) ;
#13099=PLANE ( 'NONE',  #4538 ) ;
#13163=CARTESIAN_POINT ( 'NONE',  ( 146.3141120573112630, 610.7448905601785327, 0.000000000000000000 ) ) ;
#13168=DIRECTION ( 'NONE',  ( -0.000000000000000000, -1.000000000000000000, -0.000000000000000000 ) ) ;
#13201=CYLINDRICAL_SURFACE ( 'NONE', #5979, 15.00000000000000000 ) ;
#13204=ORIENTED_EDGE ( 'NONE', *, *, #12757, .F. ) ;
#13220=DIRECTION ( 'NONE',  ( -0.000000000000000000, -1.000000000000000000, 0.000000000000000000 ) ) ;
#13225=LINE ( 'NONE', #6286, #17524 ) ;
#13254=LINE ( 'NONE', #5017, #3354 ) ;
#13294=DIRECTION ( 'NONE',  ( 0.000000000000000000, 0.000000000000000000, 1.000000000000000000 ) ) ;
#13359=DIRECTION ( 'NONE',  ( 1.191790137725560488E-16, -1.000000000000000000, -0.000000000000000000 ) ) ;
#13364=DIRECTION ( 'NONE',  ( 1.191790137725560488E-16, -1.000000000000000000, -0.000000000000000000 ) ) ;
#13463=ADVANCED_FACE ( 'NONE', ( #17963 ), #16579, .T. ) ;
#13468=AXIS2_PLACEMENT_3D ( 'NONE', #14739, #13220, #19808 ) ;
#13474=VERTEX_POINT ( 'NONE', #14642 ) ;
#13538=ORIENTED_EDGE ( 'NONE', *, *, #5202, .T. ) ;
#13554=EDGE_LOOP ( 'NONE', ( #1398, #4737, #20891, #16270 ) ) ;
#13564=CARTESIAN_POINT ( 'NONE',  ( -28.68588794268874764, 575.7448905601785327, 0.000000000000000000 ) ) ;
#13582=AXIS2_PLACEMENT_3D ( 'NONE', #4718, #21270, #7953 ) ;
#13605=CARTESIAN_POINT ( 'NONE',  ( -5.502341142637708238, 600.7448905601785327, 7.573322868991241741 ) ) ;
#13697=LINE ( 'NONE', #8917, #5416 ) ;
#13698=DIRECTION ( 'NONE',  ( 0.000000000000000000, 0.000000000000000000, 1.000000000000000000 ) ) ;
#13705=AXIS2_PLACEMENT_3D ( 'NONE', #13605, #18559, #3742 ) ;
#13711=DIRECTION ( 'NONE',  ( 1.000000000000000000, 0.000000000000000000, 0.000000000000000000 ) ) ;
#13713=VECTOR ( 'NONE', #13364, 1000.000000000000000 ) ;
#13735=EDGE_CURVE ( 'NONE', #1162, #5244, #4713, .T. ) ;
#13766=VERTEX_POINT ( 'NONE', #1184 ) ;
#13797=ORIENTED_EDGE ( 'NONE', *, *, #18469, .T. ) ;
#13808=FACE_OUTER_BOUND ( 'NONE', #2533, .T. ) ;
#13881=CARTESIAN_POINT ( 'NONE',  ( -28.68588794268875475, 600.7448905601785327, 0.000000000000000000 ) ) ;
#13897=CARTESIAN_POINT ( 'NONE',  ( -174.5421710038924346, 600.7448905601785327, -96.70028278950395872 ) ) ;
#13915=CARTESIAN_POINT ( 'NONE',  ( -43.68588794268873698, 588.2448905601785327, 1.836970198721029589E-15 ) ) ;
#13940=CARTESIAN_POINT ( 'NONE',  ( -73.08746600497821078, 585.7448905601785327, -22.98912494155474207 ) ) ;
#13945=LINE ( 'NONE', #9268, #17795 ) ;
#13950=AXIS2_PLACEMENT_3D ( 'NONE', #20760, #1287, #14492 ) ;
#13956=UNCERTAINTY_MEASURE_WITH_UNIT (LENGTH_MEASURE( 1.000000000000000082E-05 ), #16948, 'distance_accuracy_value', 'NONE');
#13959=ORIENTED_EDGE ( 'NONE', *, *, #15256, .F. ) ;
#14027=CARTESIAN_POINT ( 'NONE',  ( -28.68588794268874054, 585.7448905601785327, 0.000000000000000000 ) ) ;
#14040=ORIENTED_EDGE ( 'NONE', *, *, #2820, .T. ) ;
#14080=VECTOR ( 'NONE', #17340, 1000.000000000000114 ) ;
#14082=CYLINDRICAL_SURFACE ( 'NONE', #6243, 50.00000000000000000 ) ;
#14092=EDGE_LOOP ( 'NONE', ( #9496, #3338, #79, #19143 ) ) ;
#14166=AXIS2_PLACEMENT_3D ( 'NONE', #14951, #138, #19911 ) ;
#14178=ORIENTED_EDGE ( 'NONE', *, *, #4778, .T. ) ;
#14212=DIRECTION ( 'NONE',  ( -0.000000000000000000, -1.000000000000000000, -0.000000000000000000 ) ) ;
#14216=CARTESIAN_POINT ( 'NONE',  ( -203.6858879426887654, 610.7448905601785327, 2.143131898507868248E-14 ) ) ;
#14220=VECTOR ( 'NONE', #20584, 1000.000000000000114 ) ;
#14243=DIRECTION ( 'NONE',  ( 0.000000000000000000, 1.000000000000000000, -0.000000000000000000 ) ) ;
#14244=DIRECTION ( 'NONE',  ( 0.000000000000000000, 0.000000000000000000, 1.000000000000000000 ) ) ;
#14253=EDGE_LOOP ( 'NONE', ( #8584, #16955 ) ) ;
#14268=EDGE_CURVE ( 'NONE', #5663, #2119, #12674, .T. ) ;
#14270=CIRCLE ( 'NONE', #803, 175.0000000000000284 ) ;
#14289=EDGE_LOOP ( 'NONE', ( #6540, #1501, #657, #19367 ) ) ;
#14293=CIRCLE ( 'NONE', #8050, 50.00000000000000000 ) ;
#14301=DIRECTION ( 'NONE',  ( 0.000000000000000000, 0.000000000000000000, 1.000000000000000000 ) ) ;
#14306=CIRCLE ( 'NONE', #16729, 200.0000000000000000 ) ;
#14313=ADVANCED_FACE ( 'NONE', ( #2880 ), #9565, .F. ) ;
#14314=AXIS2_PLACEMENT_3D ( 'NONE', #20744, #15886, #4304 ) ;
#14336=EDGE_LOOP ( 'NONE', ( #5284, #9258, #4118, #8324, #9118, #6333, #18271, #11439 ) ) ;
#14374=DIRECTION ( 'NONE',  ( 0.000000000000000000, 0.000000000000000000, 1.000000000000000000 ) ) ;
#14376=CYLINDRICAL_SURFACE ( 'NONE', #5605, 175.0000000000000284 ) ;
#14378=DIRECTION ( 'NONE',  ( 1.191790137725560488E-16, -1.000000000000000000, -0.000000000000000000 ) ) ;
#14386=EDGE_CURVE ( 'NONE', #3879, #19682, #3304, .T. ) ;
#14389=ORIENTED_EDGE ( 'NONE', *, *, #4601, .T. ) ;
#14397=EDGE_CURVE ( 'NONE', #11603, #14887, #10098, .T. ) ;
#14400=DIRECTION ( 'NONE',  ( 0.000000000000000000, 0.000000000000000000, 1.000000000000000000 ) ) ;
#14416=CARTESIAN_POINT ( 'NONE',  ( -20.54277306141296222, 600.7448905601785327, 49.33244044267773631 ) ) ;
#14420=VECTOR ( 'NONE', #2425, 1000.000000000000000 ) ;
#14451=DIRECTION ( 'NONE',  ( 0.000000000000000000, 0.000000000000000000, 1.000000000000000000 ) ) ;
#14452=CARTESIAN_POINT ( 'NONE',  ( -13.68588794268874054, 588.2448905601785327, 0.000000000000000000 ) ) ;
#14456=LINE ( 'NONE', #6206, #4038 ) ;
#14470=PLANE ( 'NONE',  #8990 ) ;
#14492=DIRECTION ( 'NONE',  ( 0.000000000000000000, 0.000000000000000000, 1.000000000000000000 ) ) ;
#14493=ORIENTED_EDGE ( 'NONE', *, *, #11218, .F. ) ;
#14497=VERTEX_POINT ( 'NONE', #12368 ) ;
#14527=( LENGTH_UNIT ( ) NAMED_UNIT ( * ) SI_UNIT ( .MILLI., .METRE. ) );
#14586=CYLINDRICAL_SURFACE ( 'NONE', #6275, 15.00000000000000000 ) ;
#14598=DIRECTION ( 'NONE',  ( 1.191790137725560488E-16, -1.000000000000000000, -0.000000000000000000 ) ) ;
#14622=EDGE_CURVE ( 'NONE', #12217, #12962, #19581, .T. ) ;
#14623=EDGE_LOOP ( 'NONE', ( #13959, #1263 ) ) ;
#14640=FACE_OUTER_BOUND ( 'NONE', #4185, .T. ) ;
#14642=CARTESIAN_POINT ( 'NONE',  ( 146.1533239063698772, 600.7448905601785327, 7.500000000000000000 ) ) ;
#14673=EDGE_CURVE ( 'NONE', #20490, #5907, #598, .T. ) ;
#14682=ADVANCED_FACE ( 'NONE', ( #15628, #17346 ), #2530, .T. ) ;
#14717=EDGE_CURVE ( 'NONE', #11766, #15951, #8060, .T. ) ;
#14739=CARTESIAN_POINT ( 'NONE',  ( -28.68588794268874054, 585.7448905601785327, 0.000000000000000000 ) ) ;
#14887=VERTEX_POINT ( 'NONE', #3735 ) ;
#14900=VECTOR ( 'NONE', #20845, 1000.000000000000114 ) ;
#14938=VERTEX_POINT ( 'NONE', #16841 ) ;
#14940=ORIENTED_EDGE ( 'NONE', *, *, #5344, .F. ) ;
#14951=CARTESIAN_POINT ( 'NONE',  ( -28.68588794268875475, 600.7448905601785327, 0.000000000000000000 ) ) ;
#14986=VECTOR ( 'NONE', #14598, 1000.000000000000000 ) ;
#14991=EDGE_CURVE ( 'NONE', #4497, #18564, #13697, .T. ) ;
#14993=CARTESIAN_POINT ( 'NONE',  ( -20.54277306141296222, 600.7448905601785327, 49.33244044267773631 ) ) ;
#15014=LINE ( 'NONE', #517, #11836 ) ;
#15025=DIRECTION ( 'NONE',  ( 1.191790137725560488E-16, -1.000000000000000000, -0.000000000000000000 ) ) ;
#15070=LINE ( 'NONE', #8768, #5060 ) ;
#15122=VECTOR ( 'NONE', #2315, 1000.000000000000114 ) ;
#15131=VECTOR ( 'NONE', #11827, 1000.000000000000000 ) ;
#15136=EDGE_LOOP ( 'NONE', ( #3627, #8317, #11491, #16539, #3725, #20709, #5527, #11841, #9856, #17303, #20329, #10601, #11116, #18435, #766, #19881, #3487, #12859, #18746, #18226, #11569 ) ) ;
#15173=CARTESIAN_POINT ( 'NONE',  ( -33.07955326574333554, 600.7448905601785327, -10.74819839862556314 ) ) ;
#15176=ADVANCED_FACE ( 'NONE', ( #7609 ), #6095, .T. ) ;
#15192=EDGE_CURVE ( 'NONE', #21019, #18143, #3025, .T. ) ;
#15195=LINE ( 'NONE', #16815, #15131 ) ;
#15221=DIRECTION ( 'NONE',  ( 0.000000000000000000, 1.000000000000000000, -0.000000000000000000 ) ) ;
#15256=EDGE_CURVE ( 'NONE', #19850, #14887, #2334, .T. ) ;
#15262=DIRECTION ( 'NONE',  ( -1.000000000000000000, -1.191790137725560488E-16, 0.000000000000000000 ) ) ;
#15264=VERTEX_POINT ( 'NONE', #14452 ) ;
#15273=EDGE_CURVE ( 'NONE', #9516, #15951, #4051, .T. ) ;
#15313=CIRCLE ( 'NONE', #10436, 15.00000000000000355 ) ;
#15317=ORIENTED_EDGE ( 'NONE', *, *, #9407, .F. ) ;
#15322=CARTESIAN_POINT ( 'NONE',  ( -18.81370552131602736, 585.7448905601785327, 6.112943483001358480 ) ) ;
#15339=DIRECTION ( 'NONE',  ( -0.000000000000000000, 1.000000000000000000, -0.000000000000000000 ) ) ;
#15386=DIRECTION ( 'NONE',  ( 0.000000000000000000, 0.000000000000000000, 1.000000000000000000 ) ) ;
#15392=EDGE_CURVE ( 'NONE', #2119, #13766, #15195, .T. ) ;
#15430=DIRECTION ( 'NONE',  ( 1.000000000000000000, 0.000000000000000000, 0.000000000000000000 ) ) ;
#15434=CARTESIAN_POINT ( 'NONE',  ( -28.68588794268875120, 610.7448905601785327, 0.000000000000000000 ) ) ;
#15463=AXIS2_PLACEMENT_3D ( 'NONE', #9344, #6203, #7822 ) ;
#15471=EDGE_LOOP ( 'NONE', ( #2292, #4069, #20620, #7095 ) ) ;
#15509=AXIS2_PLACEMENT_3D ( 'NONE', #9777, #7836, #19737 ) ;
#15521=AXIS2_PLACEMENT_3D ( 'NONE', #7694, #17547, #4456 ) ;
#15545=CYLINDRICAL_SURFACE ( 'NONE', #11123, 175.0000000000000284 ) ;
#15546=DIRECTION ( 'NONE',  ( -1.000000000000000000, 0.000000000000000000, 0.000000000000000000 ) ) ;
#15553=EDGE_CURVE ( 'NONE', #9225, #20381, #20303, .T. ) ;
#15559=LINE ( 'NONE', #12405, #14900 ) ;
#15582=VERTEX_POINT ( 'NONE', #8414 ) ;
#15628=FACE_OUTER_BOUND ( 'NONE', #2562, .T. ) ;
#15671=CARTESIAN_POINT ( 'NONE',  ( 158.8141120573112630, 10.52886280891152104, 10.00000000000000888 ) ) ;
#15674=EDGE_CURVE ( 'NONE', #12962, #5244, #11669, .T. ) ;
#15686=PLANE ( 'NONE',  #12206 ) ;
#15687=VERTEX_POINT ( 'NONE', #111 ) ;
#15706=VERTEX_POINT ( 'NONE', #20294 ) ;
#15712=ORIENTED_EDGE ( 'NONE', *, *, #16152, .F. ) ;
#15719=DIRECTION ( 'NONE',  ( 0.000000000000000000, 1.000000000000000000, -0.000000000000000000 ) ) ;
#15734=DIRECTION ( 'NONE',  ( 0.000000000000000000, 1.000000000000000000, -0.000000000000000000 ) ) ;
#15750=LINE ( 'NONE', #5996, #11003 ) ;
#15814=FACE_OUTER_BOUND ( 'NONE', #11350, .T. ) ;
#15823=DIRECTION ( 'NONE',  ( 0.000000000000000000, 1.000000000000000000, -0.000000000000000000 ) ) ;
#15827=CARTESIAN_POINT ( 'NONE',  ( -28.68588794268875120, 585.7448905601785327, 0.000000000000000000 ) ) ;
#15846=EDGE_CURVE ( 'NONE', #11996, #15687, #21036, .T. ) ;
#15854=EDGE_LOOP ( 'NONE', ( #1095, #10682 ) ) ;
#15868=DIRECTION ( 'NONE',  ( 0.000000000000000000, 1.000000000000000000, -0.000000000000000000 ) ) ;
#15886=DIRECTION ( 'NONE',  ( 0.000000000000000000, 1.000000000000000000, -0.000000000000000000 ) ) ;
#15901=CARTESIAN_POINT ( 'NONE',  ( -64.27068722059112815, 585.7448905601785327, -35.12437985717895828 ) ) ;
#15907=LINE ( 'NONE', #10805, #4818 ) ;
#15939=DIRECTION ( 'NONE',  ( -0.000000000000000000, -1.000000000000000000, -0.000000000000000000 ) ) ;
#15951=VERTEX_POINT ( 'NONE', #2552 ) ;
#15967=DIRECTION ( 'NONE',  ( 0.000000000000000000, 1.000000000000000000, -0.000000000000000000 ) ) ;
#15971=EDGE_CURVE ( 'NONE', #1814, #12774, #1627, .T. ) ;
#15983=EDGE_CURVE ( 'NONE', #2560, #15706, #266, .T. ) ;
#15987=EDGE_CURVE ( 'NONE', #6213, #4291, #14456, .T. ) ;
#15991=ADVANCED_FACE ( 'NONE', ( #9769 ), #11617, .F. ) ;
#16020=CARTESIAN_POINT ( 'NONE',  ( -28.68588794268875120, 610.7448905601785327, 0.000000000000000000 ) ) ;
#16060=DIRECTION ( 'NONE',  ( 1.191790137725560488E-16, -1.000000000000000000, -0.000000000000000000 ) ) ;
#16073=CARTESIAN_POINT ( 'NONE',  ( -28.68588794268874054, 600.7448905601785327, 20.00000000000000355 ) ) ;
#16076=DIRECTION ( 'NONE',  ( 0.8090169943749473402, 0.000000000000000000, -0.5877852522924732481 ) ) ;
#16091=CYLINDRICAL_SURFACE ( 'NONE', #2373, 50.00000000000000000 ) ;
#16093=CARTESIAN_POINT ( 'NONE',  ( 158.8141120573112630, 575.7448905601785327, 10.00000000000000888 ) ) ;
#16124=CARTESIAN_POINT ( 'NONE',  ( 20.74841189052421697, 600.7448905601785327, -7.500000000000000000 ) ) ;
#16139=CARTESIAN_POINT ( 'NONE',  ( -8.685887942688735208, 585.7448905601785327, 0.000000000000000000 ) ) ;
#16152=EDGE_CURVE ( 'NONE', #11679, #20997, #20275, .T. ) ;
#16158=AXIS2_PLACEMENT_3D ( 'NONE', #16363, #19592, #4771 ) ;
#16164=CARTESIAN_POINT ( 'NONE',  ( 146.3141120573112630, 610.7448905601785327, 0.000000000000000000 ) ) ;
#16174=CARTESIAN_POINT ( 'NONE',  ( -28.68588794268875120, 585.7448905601785327, 0.000000000000000000 ) ) ;
#16205=DIRECTION ( 'NONE',  ( 1.000000000000000000, 0.000000000000000000, 0.000000000000000000 ) ) ;
#16208=EDGE_CURVE ( 'NONE', #9825, #4497, #13254, .T. ) ;
#16227=DIRECTION ( 'NONE',  ( -1.191790137725560488E-16, 1.000000000000000000, 0.000000000000000000 ) ) ;
#16234=LINE ( 'NONE', #4749, #9080 ) ;
#16240=ORIENTED_EDGE ( 'NONE', *, *, #19316, .T. ) ;
#16270=ORIENTED_EDGE ( 'NONE', *, *, #15392, .T. ) ;
#16272=AXIS2_PLACEMENT_3D ( 'NONE', #13881, #15719, #7468 ) ;
#16287=CIRCLE ( 'NONE', #64, 10.00000000000000888 ) ;
#16297=PLANE ( 'NONE',  #15509 ) ;
#16310=LINE ( 'NONE', #13163, #17912 ) ;
#16313=DIRECTION ( 'NONE',  ( 1.000000000000000000, 0.000000000000000000, 0.000000000000000000 ) ) ;
#16321=EDGE_CURVE ( 'NONE', #13474, #11682, #18194, .T. ) ;
#16340=PRODUCT_DEFINITION_SHAPE ( 'NONE', 'NONE',  #7228 ) ;
#16341=AXIS2_PLACEMENT_3D ( 'NONE', #5256, #15221, #18345 ) ;
#16363=CARTESIAN_POINT ( 'NONE',  ( -28.68588794268875475, 600.7448905601785327, 0.000000000000000000 ) ) ;
#16366=DIRECTION ( 'NONE',  ( 0.000000000000000000, 1.000000000000000000, -0.000000000000000000 ) ) ;
#16413=DIRECTION ( 'NONE',  ( 1.191790137725560488E-16, -1.000000000000000000, -0.000000000000000000 ) ) ;
#16439=EDGE_CURVE ( 'NONE', #18143, #14497, #10512, .T. ) ;
#16499=CARTESIAN_POINT ( 'NONE',  ( -33.07955326574332133, 600.7448905601785327, 10.74819839862556492 ) ) ;
#16507=EDGE_CURVE ( 'NONE', #3879, #11996, #9214, .T. ) ;
#16514=CARTESIAN_POINT ( 'NONE',  ( -28.68588794268874054, 608.2448905601786464, 20.00000000000000000 ) ) ;
#16516=ORIENTED_EDGE ( 'NONE', *, *, #16208, .T. ) ;
#16518=CARTESIAN_POINT ( 'NONE',  ( -43.68588794268873698, 588.2448905601785327, 1.836970198721029589E-15 ) ) ;
#16539=ORIENTED_EDGE ( 'NONE', *, *, #5565, .F. ) ;
#16556=EDGE_LOOP ( 'NONE', ( #17804, #7357, #11597, #3673 ) ) ;
#16559=CARTESIAN_POINT ( 'NONE',  ( -28.68588794268875120, 585.7448905601785327, 0.000000000000000000 ) ) ;
#16579=PLANE ( 'NONE',  #1606 ) ;
#16580=DIRECTION ( 'NONE',  ( 0.000000000000000000, 1.000000000000000000, -0.000000000000000000 ) ) ;
#16599=ADVANCED_FACE ( 'NONE', ( #12583 ), #17550, .T. ) ;
#16603=CARTESIAN_POINT ( 'NONE',  ( -14.31911992702480241, 600.7448905601785327, 19.70857778461545351 ) ) ;
#16657=EDGE_CURVE ( 'NONE', #5663, #14938, #13225, .T. ) ;
#16687=CARTESIAN_POINT ( 'NONE',  ( -28.68588794268874409, 608.2448905601786464, 0.000000000000000000 ) ) ;
#16723=ADVANCED_FACE ( 'NONE', ( #19696 ), #19813, .T. ) ;
#16729=AXIS2_PLACEMENT_3D ( 'NONE', #8907, #10740, #9229 ) ;
#16770=CYLINDRICAL_SURFACE ( 'NONE', #204, 10.00000000000000888 ) ;
#16782=ORIENTED_EDGE ( 'NONE', *, *, #21383, .F. ) ;
#16792=DIRECTION ( 'NONE',  ( 0.000000000000000000, 0.000000000000000000, 1.000000000000000000 ) ) ;
#16797=ORIENTED_EDGE ( 'NONE', *, *, #5110, .F. ) ;
#16815=CARTESIAN_POINT ( 'NONE',  ( -6.276925316985672687, 600.7448905601785327, -44.69718552705352721 ) ) ;
#16841=CARTESIAN_POINT ( 'NONE',  ( 20.74841189052422052, 585.7448905601785327, -7.500000000000000000 ) ) ;
#16844=ADVANCED_FACE ( 'NONE', ( #14640 ), #13001, .T. ) ;
#16854=CARTESIAN_POINT ( 'NONE',  ( -28.68588794268875120, 610.7448905601785327, 0.000000000000000000 ) ) ;
#16877=ORIENTED_EDGE ( 'NONE', *, *, #17558, .F. ) ;
#16934=ORIENTED_EDGE ( 'NONE', *, *, #20866, .F. ) ;
#16946=DIRECTION ( 'NONE',  ( 0.000000000000000000, 1.000000000000000000, -0.000000000000000000 ) ) ;
#16948=( LENGTH_UNIT ( ) NAMED_UNIT ( * ) SI_UNIT ( .MILLI., .METRE. ) );
#16951=CYLINDRICAL_SURFACE ( 'NONE', #3003, 10.00000000000000888 ) ;
#16955=ORIENTED_EDGE ( 'NONE', *, *, #20481, .F. ) ;
#16959=EDGE_CURVE ( 'NONE', #14497, #289, #12120, .T. ) ;
#16985=FACE_BOUND ( 'NONE', #19209, .T. ) ;
#17031=EDGE_CURVE ( 'NONE', #10415, #11766, #2499, .T. ) ;
#17038=EDGE_LOOP ( 'NONE', ( #18610, #10447, #2044, #6937 ) ) ;
#17080=CIRCLE ( 'NONE', #17764, 175.0000000000000284 ) ;
#17090=ORIENTED_EDGE ( 'NONE', *, *, #8743, .T. ) ;
#17102=FACE_OUTER_BOUND ( 'NONE', #12245, .T. ) ;
#17135=CARTESIAN_POINT ( 'NONE',  ( -5.502341142637708238, 600.7448905601785327, 7.573322868991241741 ) ) ;
#17150=ORIENTED_EDGE ( 'NONE', *, *, #9223, .F. ) ;
#17156=CARTESIAN_POINT ( 'NONE',  ( -28.68588794268875120, 585.7448905601785327, 0.000000000000000000 ) ) ;
#17175=ORIENTED_EDGE ( 'NONE', *, *, #21383, .T. ) ;
#17176=CARTESIAN_POINT ( 'NONE',  ( -5.502341142637706461, 585.7448905601785327, 7.573322868991241741 ) ) ;
#17178=ORIENTED_EDGE ( 'NONE', *, *, #8344, .T. ) ;
#17180=AXIS2_PLACEMENT_3D ( 'NONE', #3404, #17888, #8139 ) ;
#17212=PRODUCT_DEFINITION_CONTEXT ( 'detailed design', #4184, 'design' ) ;
#17242=DIRECTION ( 'NONE',  ( 0.000000000000000000, 0.000000000000000000, 1.000000000000000000 ) ) ;
#17259=CARTESIAN_POINT ( 'NONE',  ( -28.68588794268875120, 585.7448905601785327, 0.000000000000000000 ) ) ;
#17263=DIRECTION ( 'NONE',  ( 1.191790137725560488E-16, -1.000000000000000000, -0.000000000000000000 ) ) ;
#17264=FACE_BOUND ( 'NONE', #10024, .T. ) ;
#17281=FACE_OUTER_BOUND ( 'NONE', #19474, .T. ) ;
#17303=ORIENTED_EDGE ( 'NONE', *, *, #11824, .T. ) ;
#17324=ORIENTED_EDGE ( 'NONE', *, *, #15983, .T. ) ;
#17340=DIRECTION ( 'NONE',  ( 0.3090169943749473958, 0.000000000000000000, 0.9510565162951535312 ) ) ;
#17346=FACE_BOUND ( 'NONE', #14253, .T. ) ;
#17374=EDGE_CURVE ( 'NONE', #19682, #15687, #11129, .T. ) ;
#17415=VERTEX_POINT ( 'NONE', #3133 ) ;
#17426=EDGE_CURVE ( 'NONE', #15264, #8423, #11310, .T. ) ;
#17430=ORIENTED_EDGE ( 'NONE', *, *, #14397, .F. ) ;
#17456=DIRECTION ( 'NONE',  ( 1.191790137725560488E-16, -1.000000000000000000, -0.000000000000000000 ) ) ;
#17478=EDGE_LOOP ( 'NONE', ( #8533, #9391, #2890, #16516 ) ) ;
#17524=VECTOR ( 'NONE', #142, 1000.000000000000000 ) ;
#17531=AXIS2_PLACEMENT_3D ( 'NONE', #16020, #7772, #14400 ) ;
#17537=CIRCLE ( 'NONE', #18567, 175.0000000000000284 ) ;
#17547=DIRECTION ( 'NONE',  ( 0.000000000000000000, 1.000000000000000000, -0.000000000000000000 ) ) ;
#17550=CYLINDRICAL_SURFACE ( 'NONE', #5424, 20.00000000000000000 ) ;
#17558=EDGE_CURVE ( 'NONE', #20381, #9225, #17537, .T. ) ;
#17598=CARTESIAN_POINT ( 'NONE',  ( -28.68588794268875475, 600.7448905601785327, 0.000000000000000000 ) ) ;
#17615=ORIENTED_EDGE ( 'NONE', *, *, #18931, .F. ) ;
#17671=ORIENTED_EDGE ( 'NONE', *, *, #5335, .T. ) ;
#17677=CIRCLE ( 'NONE', #20442, 10.00000000000000888 ) ;
#17685=LINE ( 'NONE', #10094, #11431 ) ;
#17703=DIRECTION ( 'NONE',  ( 1.191790137725560488E-16, -1.000000000000000000, -0.000000000000000000 ) ) ;
#17732=AXIS2_PLACEMENT_3D ( 'NONE', #17156, #16946, #13698 ) ;
#17739=CARTESIAN_POINT ( 'NONE',  ( -18.81370552131603091, 600.7448905601785327, 6.112943483001358480 ) ) ;
#17745=ORIENTED_EDGE ( 'NONE', *, *, #6774, .T. ) ;
#17764=AXIS2_PLACEMENT_3D ( 'NONE', #9306, #15823, #12246 ) ;
#17785=DIRECTION ( 'NONE',  ( 1.191790137725560488E-16, -1.000000000000000000, -0.000000000000000000 ) ) ;
#17795=VECTOR ( 'NONE', #18895, 1000.000000000000000 ) ;
#17804=ORIENTED_EDGE ( 'NONE', *, *, #12135, .F. ) ;
#17888=DIRECTION ( 'NONE',  ( 0.000000000000000000, 1.000000000000000000, 0.000000000000000000 ) ) ;
#17896=FACE_OUTER_BOUND ( 'NONE', #12801, .T. ) ;
#17910=FACE_BOUND ( 'NONE', #15471, .T. ) ;
#17912=VECTOR ( 'NONE', #16413, 1000.000000000000000 ) ;
#17922=VECTOR ( 'NONE', #14212, 1000.000000000000000 ) ;
#17944=ORIENTED_EDGE ( 'NONE', *, *, #12663, .F. ) ;
#17952=CARTESIAN_POINT ( 'NONE',  ( -28.68588794268874054, 588.2448905601785327, 0.000000000000000000 ) ) ;
#17963=FACE_OUTER_BOUND ( 'NONE', #11271, .T. ) ;
#17971=ORIENTED_EDGE ( 'NONE', *, *, #4719, .T. ) ;
#17992=CARTESIAN_POINT ( 'NONE',  ( -8.685887942688735208, 588.2448905601785327, 0.000000000000000000 ) ) ;
#17998=CARTESIAN_POINT ( 'NONE',  ( -28.68588794268875475, 600.7448905601785327, 0.000000000000000000 ) ) ;
#18022=LINE ( 'NONE', #3216, #20523 ) ;
#18024=LINE ( 'NONE', #19645, #5938 ) ;
#18049=DIRECTION ( 'NONE',  ( 0.3090169943749473958, 0.000000000000000000, 0.9510565162951535312 ) ) ;
#18052=FACE_OUTER_BOUND ( 'NONE', #7412, .T. ) ;
#18073=ADVANCED_FACE ( 'NONE', ( #2034 ), #418, .F. ) ;
#18075=ADVANCED_FACE ( 'NONE', ( #10329 ), #16951, .F. ) ;
#18088=CARTESIAN_POINT ( 'NONE',  ( -228.6858879426887654, 575.7448905601785327, 2.449293598294706434E-14 ) ) ;
#18116=FACE_OUTER_BOUND ( 'NONE', #6090, .T. ) ;
#18123=DIRECTION ( 'NONE',  ( -1.191790137725560488E-16, 1.000000000000000000, 0.000000000000000000 ) ) ;
#18143=VERTEX_POINT ( 'NONE', #20514 ) ;
#18162=DIRECTION ( 'NONE',  ( 0.000000000000000000, 0.000000000000000000, 1.000000000000000000 ) ) ;
#18184=DIRECTION ( 'NONE',  ( 0.000000000000000000, 0.000000000000000000, 1.000000000000000000 ) ) ;
#18194=CIRCLE ( 'NONE', #8866, 175.0000000000000284 ) ;
#18211=DIRECTION ( 'NONE',  ( 1.191790137725560488E-16, -1.000000000000000000, -0.000000000000000000 ) ) ;
#18225=EDGE_CURVE ( 'NONE', #14938, #2589, #20936, .T. ) ;
#18226=ORIENTED_EDGE ( 'NONE', *, *, #11483, .F. ) ;
#18271=ORIENTED_EDGE ( 'NONE', *, *, #8244, .T. ) ;
#18289=EDGE_CURVE ( 'NONE', #6118, #6933, #2309, .T. ) ;
#18317=VECTOR ( 'NONE', #4909, 1000.000000000000114 ) ;
#18345=DIRECTION ( 'NONE',  ( 0.000000000000000000, 0.000000000000000000, 1.000000000000000000 ) ) ;
#18378=ORIENTED_EDGE ( 'NONE', *, *, #8244, .F. ) ;
#18405=CARTESIAN_POINT ( 'NONE',  ( 32.47532367400565079, 585.7448905601785327, -163.9643442751439864 ) ) ;
#18408=AXIS2_PLACEMENT_3D ( 'NONE', #2183, #3899, #15386 ) ;
#18409=EDGE_CURVE ( 'NONE', #8588, #6213, #7115, .T. ) ;
#18435=ORIENTED_EDGE ( 'NONE', *, *, #11471, .T. ) ;
#18452=CARTESIAN_POINT ( 'NONE',  ( -28.68588794268875475, 600.7448905601785327, 0.000000000000000000 ) ) ;
#18469=EDGE_CURVE ( 'NONE', #8588, #6162, #15070, .T. ) ;
#18478=ADVANCED_FACE ( 'NONE', ( #7031 ), #7239, .T. ) ;
#18505=ORIENTED_EDGE ( 'NONE', *, *, #15674, .T. ) ;
#18532=DIRECTION ( 'NONE',  ( 0.000000000000000000, 0.000000000000000000, 1.000000000000000000 ) ) ;
#18553=DIRECTION ( 'NONE',  ( 1.191790137725560488E-16, -1.000000000000000000, -0.000000000000000000 ) ) ;
#18554=AXIS2_PLACEMENT_3D ( 'NONE', #21327, #5096, #11698 ) ;
#18559=DIRECTION ( 'NONE',  ( -0.5877852522924731371, -7.005166667826997985E-17, 0.8090169943749475623 ) ) ;
#18564=VERTEX_POINT ( 'NONE', #1981 ) ;
#18567=AXIS2_PLACEMENT_3D ( 'NONE', #3663, #8740, #20001 ) ;
#18568=ORIENTED_EDGE ( 'NONE', *, *, #18409, .T. ) ;
#18585=DIRECTION ( 'NONE',  ( 0.000000000000000000, 0.000000000000000000, 1.000000000000000000 ) ) ;
#18593=ORIENTED_EDGE ( 'NONE', *, *, #15846, .F. ) ;
#18610=ORIENTED_EDGE ( 'NONE', *, *, #11824, .F. ) ;
#18619=CARTESIAN_POINT ( 'NONE',  ( -73.08746600497821078, 600.7448905601785327, -22.98912494155474207 ) ) ;
#18647=EDGE_CURVE ( 'NONE', #10685, #19682, #815, .T. ) ;
#18652=DIRECTION ( 'NONE',  ( -1.191790137725560488E-16, 1.000000000000000000, 0.000000000000000000 ) ) ;
#18654=FACE_BOUND ( 'NONE', #12753, .T. ) ;
#18664=VECTOR ( 'NONE', #11505, 1000.000000000000000 ) ;
#18672=EDGE_LOOP ( 'NONE', ( #17150, #14940, #101, #10905 ) ) ;
#18679=AXIS2_PLACEMENT_3D ( 'NONE', #19116, #10882, #20850 ) ;
#18738=DIRECTION ( 'NONE',  ( 0.000000000000000000, 1.000000000000000000, -0.000000000000000000 ) ) ;
#18746=ORIENTED_EDGE ( 'NONE', *, *, #19316, .F. ) ;
#18758=CIRCLE ( 'NONE', #13950, 175.0000000000000284 ) ;
#18780=LINE ( 'NONE', #17176, #11053 ) ;
#18785=DIRECTION ( 'NONE',  ( -0.000000000000000000, 1.000000000000000000, -0.000000000000000000 ) ) ;
#18800=CARTESIAN_POINT ( 'NONE',  ( -174.5421710038924061, 600.7448905601785327, 96.70028278950401557 ) ) ;
#18818=DIRECTION ( 'NONE',  ( -0.9510565162951536422, -1.133459776540192663E-16, -0.3090169943749472292 ) ) ;
#18819=ADVANCED_FACE ( 'NONE', ( #18052 ), #13201, .F. ) ;
#18829=PLANE ( 'NONE',  #5672 ) ;
#18847=SHAPE_REPRESENTATION ( 'Heavy Perimeter Inertia Flywheel Disk', ( #12794 ), #20056 ) ;
#18854=DIRECTION ( 'NONE',  ( 0.3090169943749475068, 0.000000000000000000, 0.9510565162951535312 ) ) ;
#18880=EDGE_CURVE ( 'NONE', #5244, #9516, #16234, .T. ) ;
#18895=DIRECTION ( 'NONE',  ( -0.000000000000000000, 1.000000000000000000, -0.000000000000000000 ) ) ;
#18909=ORIENTED_EDGE ( 'NONE', *, *, #10014, .F. ) ;
#18931=EDGE_CURVE ( 'NONE', #10415, #3879, #1851, .T. ) ;
#18936=DIRECTION ( 'NONE',  ( 0.000000000000000000, 0.000000000000000000, -1.000000000000000000 ) ) ;
#18956=CARTESIAN_POINT ( 'NONE',  ( -28.68588794268875475, 600.7448905601785327, 0.000000000000000000 ) ) ;
#18991=ORIENTED_EDGE ( 'NONE', *, *, #16959, .T. ) ;
#18997=CARTESIAN_POINT ( 'NONE',  ( -203.6858879426887654, 575.7448905601785327, 2.143131898507868248E-14 ) ) ;
#19029=ORIENTED_EDGE ( 'NONE', *, *, #7307, .F. ) ;
#19097=DIRECTION ( 'NONE',  ( 0.000000000000000000, 0.000000000000000000, 1.000000000000000000 ) ) ;
#19116=CARTESIAN_POINT ( 'NONE',  ( -5.502341142637721561, 600.7448905601785327, -7.573322868991255952 ) ) ;
#19118=CARTESIAN_POINT ( 'NONE',  ( 32.47532367400570763, 585.7448905601785327, 163.9643442751439295 ) ) ;
#19143=ORIENTED_EDGE ( 'NONE', *, *, #8010, .F. ) ;
#19198=DIRECTION ( 'NONE',  ( 0.000000000000000000, 0.000000000000000000, 1.000000000000000000 ) ) ;
#19209=EDGE_LOOP ( 'NONE', ( #19417, #17745 ) ) ;
#19275=CARTESIAN_POINT ( 'NONE',  ( 146.3141120573112630, 610.7448905601785327, 0.000000000000000000 ) ) ;
#19316=EDGE_CURVE ( 'NONE', #289, #5907, #8054, .T. ) ;
#19320=EDGE_LOOP ( 'NONE', ( #2779, #18568 ) ) ;
#19367=ORIENTED_EDGE ( 'NONE', *, *, #21219, .F. ) ;
#19417=ORIENTED_EDGE ( 'NONE', *, *, #12595, .T. ) ;
#19459=DIRECTION ( 'NONE',  ( -1.000000000000000000, 0.000000000000000000, 0.000000000000000000 ) ) ;
#19465=DIRECTION ( 'NONE',  ( 1.191790137725560488E-16, -1.000000000000000000, -0.000000000000000000 ) ) ;
#19468=DIRECTION ( 'NONE',  ( -0.3090169943749475068, 0.000000000000000000, -0.9510565162951535312 ) ) ;
#19471=VECTOR ( 'NONE', #18854, 1000.000000000000114 ) ;
#19474=EDGE_LOOP ( 'NONE', ( #4578, #9940, #9776, #3334 ) ) ;
#19475=DIRECTION ( 'NONE',  ( -1.000000000000000000, -1.191790137725560488E-16, 0.000000000000000000 ) ) ;
#19565=DIRECTION ( 'NONE',  ( -1.000000000000000000, 0.000000000000000000, 0.000000000000000000 ) ) ;
#19567=CARTESIAN_POINT ( 'NONE',  ( -28.68588794268874054, 588.2448905601785327, 0.000000000000000000 ) ) ;
#19573=EDGE_LOOP ( 'NONE', ( #7568, #14493, #9412, #17324 ) ) ;
#19575=ORIENTED_EDGE ( 'NONE', *, *, #3372, .F. ) ;
#19581=CIRCLE ( 'NONE', #11970, 50.00000000000000000 ) ;
#19592=DIRECTION ( 'NONE',  ( 1.191790137725560488E-16, -1.000000000000000000, -0.000000000000000000 ) ) ;
#19597=VECTOR ( 'NONE', #20083, 1000.000000000000000 ) ;
#19627=ORIENTED_EDGE ( 'NONE', *, *, #2237, .T. ) ;
#19637=LINE ( 'NONE', #16518, #12471 ) ;
#19645=CARTESIAN_POINT ( 'NONE',  ( 146.1533239063698772, 600.7448905601785327, 7.500000000000000000 ) ) ;
#19667=LINE ( 'NONE', #4961, #5165 ) ;
#19682=VERTEX_POINT ( 'NONE', #19945 ) ;
#19696=FACE_OUTER_BOUND ( 'NONE', #18672, .T. ) ;
#19706=ORIENTED_EDGE ( 'NONE', *, *, #21068, .T. ) ;
#19726=LINE ( 'NONE', #16603, #18317 ) ;
#19728=CIRCLE ( 'NONE', #20412, 15.00000000000000000 ) ;
#19737=DIRECTION ( 'NONE',  ( 0.000000000000000000, -0.000000000000000000, 1.000000000000000000 ) ) ;
#19755=( NAMED_UNIT ( * ) SI_UNIT ( $, .STERADIAN. ) SOLID_ANGLE_UNIT ( ) );
#19808=DIRECTION ( 'NONE',  ( 0.000000000000000000, 0.000000000000000000, 1.000000000000000000 ) ) ;
#19813=CYLINDRICAL_SURFACE ( 'NONE', #18554, 20.00000000000000000 ) ;
#19850=VERTEX_POINT ( 'NONE', #5014 ) ;
#19881=ORIENTED_EDGE ( 'NONE', *, *, #18880, .F. ) ;
#19896=ORIENTED_EDGE ( 'NONE', *, *, #18409, .F. ) ;
#19911=DIRECTION ( 'NONE',  ( 1.000000000000000000, 0.000000000000000000, 0.000000000000000000 ) ) ;
#19945=CARTESIAN_POINT ( 'NONE',  ( -20.54277306141295867, 585.7448905601785327, 49.33244044267773631 ) ) ;
#19949=DIRECTION ( 'NONE',  ( 0.9510565162951536422, 1.133459776540192910E-16, -0.3090169943749473958 ) ) ;
#19955=CARTESIAN_POINT ( 'NONE',  ( -48.68588794268874409, 588.2448905601785327, 2.449293598294706907E-15 ) ) ;
#20001=DIRECTION ( 'NONE',  ( 0.000000000000000000, 0.000000000000000000, 1.000000000000000000 ) ) ;
#20056=( GEOMETRIC_REPRESENTATION_CONTEXT ( 3 ) GLOBAL_UNCERTAINTY_ASSIGNED_CONTEXT ( ( #11591 ) ) GLOBAL_UNIT_ASSIGNED_CONTEXT ( ( #14527, #21010, #9529 ) ) REPRESENTATION_CONTEXT ( 'NONE', 'WORKASPACE' ) );
#20083=DIRECTION ( 'NONE',  ( 1.191790137725560488E-16, -1.000000000000000000, -0.000000000000000000 ) ) ;
#20143=EDGE_LOOP ( 'NONE', ( #3746, #2609 ) ) ;
#20152=DIRECTION ( 'NONE',  ( 0.000000000000000000, 1.000000000000000000, -0.000000000000000000 ) ) ;
#20275=CIRCLE ( 'NONE', #17180, 20.00000000000000000 ) ;
#20287=AXIS2_PLACEMENT_3D ( 'NONE', #16174, #11072, #21032 ) ;
#20289=CARTESIAN_POINT ( 'NONE',  ( -228.6858879426887654, 610.7448905601785327, 2.449293598294706434E-14 ) ) ;
#20294=CARTESIAN_POINT ( 'NONE',  ( 158.8141120573112630, 610.7448905601785327, -10.00000000000000888 ) ) ;
#20298=DIRECTION ( 'NONE',  ( 0.000000000000000000, 0.000000000000000000, 1.000000000000000000 ) ) ;
#20303=CIRCLE ( 'NONE', #17531, 175.0000000000000284 ) ;
#20322=CARTESIAN_POINT ( 'NONE',  ( 158.8141120573112630, 10.52886280891152104, 0.000000000000000000 ) ) ;
#20329=ORIENTED_EDGE ( 'NONE', *, *, #733, .F. ) ;
#20333=VERTEX_POINT ( 'NONE', #16093 ) ;
#20354=DIRECTION ( 'NONE',  ( 1.191790137725560488E-16, -1.000000000000000000, -0.000000000000000000 ) ) ;
#20381=VERTEX_POINT ( 'NONE', #11315 ) ;
#20388=ORIENTED_EDGE ( 'NONE', *, *, #5344, .T. ) ;
#20412=AXIS2_PLACEMENT_3D ( 'NONE', #7404, #519, #15546 ) ;
#20435=ORIENTED_EDGE ( 'NONE', *, *, #14622, .F. ) ;
#20442=AXIS2_PLACEMENT_3D ( 'NONE', #1722, #1610, #13294 ) ;
#20459=AXIS2_PLACEMENT_3D ( 'NONE', #17998, #15967, #3081 ) ;
#20468=ADVANCED_FACE ( 'NONE', ( #9794, #17910, #4618 ), #14376, .F. ) ;
#20481=EDGE_CURVE ( 'NONE', #12774, #1814, #12876, .T. ) ;
#20490=VERTEX_POINT ( 'NONE', #6128 ) ;
#20514=CARTESIAN_POINT ( 'NONE',  ( -64.27068722059112815, 600.7448905601785327, -35.12437985717895828 ) ) ;
#20521=ORIENTED_EDGE ( 'NONE', *, *, #18647, .T. ) ;
#20523=VECTOR ( 'NONE', #13168, 1000.000000000000000 ) ;
#20531=LINE ( 'NONE', #15671, #10993 ) ;
#20574=CARTESIAN_POINT ( 'NONE',  ( -18.81370552131602736, 600.7448905601785327, -6.112943483001347822 ) ) ;
#20584=DIRECTION ( 'NONE',  ( -0.8090169943749474513, 0.000000000000000000, -0.5877852522924730261 ) ) ;
#20585=CARTESIAN_POINT ( 'NONE',  ( -73.08746600497821078, 600.7448905601785327, 22.98912494155475628 ) ) ;
#20595=LINE ( 'NONE', #823, #19471 ) ;
#20608=CARTESIAN_POINT ( 'NONE',  ( -73.08746600497821078, 600.7448905601785327, 22.98912494155475628 ) ) ;
#20609=CARTESIAN_POINT ( 'NONE',  ( 20.74841189052422052, 585.7448905601785327, 7.500000000000000000 ) ) ;
#20620=ORIENTED_EDGE ( 'NONE', *, *, #733, .T. ) ;
#20628=AXIS2_PLACEMENT_3D ( 'NONE', #10863, #14243, #7724 ) ;
#20647=ORIENTED_EDGE ( 'NONE', *, *, #15192, .T. ) ;
#20655=ORIENTED_EDGE ( 'NONE', *, *, #21120, .F. ) ;
#20663=EDGE_CURVE ( 'NONE', #18143, #10958, #15014, .T. ) ;
#20709=ORIENTED_EDGE ( 'NONE', *, *, #20775, .F. ) ;
#20744=CARTESIAN_POINT ( 'NONE',  ( -28.68588794268875475, 600.7448905601785327, 0.000000000000000000 ) ) ;
#20760=CARTESIAN_POINT ( 'NONE',  ( -28.68588794268874764, 575.7448905601785327, 0.000000000000000000 ) ) ;
#20762=ORIENTED_EDGE ( 'NONE', *, *, #20866, .T. ) ;
#20775=EDGE_CURVE ( 'NONE', #7989, #2589, #3551, .T. ) ;
#20803=DIRECTION ( 'NONE',  ( 1.191790137725560488E-16, -1.000000000000000000, -0.000000000000000000 ) ) ;
#20805=( GEOMETRIC_REPRESENTATION_CONTEXT ( 3 ) GLOBAL_UNCERTAINTY_ASSIGNED_CONTEXT ( ( #13956 ) ) GLOBAL_UNIT_ASSIGNED_CONTEXT ( ( #16948, #4939, #19755 ) ) REPRESENTATION_CONTEXT ( 'NONE', 'WORKASPACE' ) );
#20806=EDGE_CURVE ( 'NONE', #11682, #6477, #14270, .T. ) ;
#20826=DIRECTION ( 'NONE',  ( 1.191790137725560488E-16, -1.000000000000000000, -0.000000000000000000 ) ) ;
#20845=DIRECTION ( 'NONE',  ( -0.8090169943749473402, 0.000000000000000000, 0.5877852522924733591 ) ) ;
#20850=DIRECTION ( 'NONE',  ( 0.8090169943749473402, 0.000000000000000000, -0.5877852522924733591 ) ) ;
#20866=EDGE_CURVE ( 'NONE', #827, #11603, #8726, .T. ) ;
#20891=ORIENTED_EDGE ( 'NONE', *, *, #522, .F. ) ;
#20933=EDGE_CURVE ( 'NONE', #17415, #10551, #15313, .T. ) ;
#20936=LINE ( 'NONE', #11370, #1978 ) ;
#20940=ORIENTED_EDGE ( 'NONE', *, *, #11483, .T. ) ;
#20947=CARTESIAN_POINT ( 'NONE',  ( 146.3141120573112630, 600.7448905601785327, 0.000000000000000000 ) ) ;
#20957=CARTESIAN_POINT ( 'NONE',  ( -28.68588794268875120, 610.7448905601785327, 0.000000000000000000 ) ) ;
#20965=CARTESIAN_POINT ( 'NONE',  ( -28.68588794268875120, 585.7448905601785327, 0.000000000000000000 ) ) ;
#20967=AXIS2_PLACEMENT_3D ( 'NONE', #20965, #3223, #6448 ) ;
#20984=VECTOR ( 'NONE', #18049, 1000.000000000000114 ) ;
#20997=VERTEX_POINT ( 'NONE', #1567 ) ;
#20998=FACE_BOUND ( 'NONE', #20143, .T. ) ;
#21010=( NAMED_UNIT ( * ) PLANE_ANGLE_UNIT ( ) SI_UNIT ( $, .RADIAN. ) );
#21013=LINE ( 'NONE', #6182, #9351 ) ;
#21019=VERTEX_POINT ( 'NONE', #11391 ) ;
#21027=ORIENTED_EDGE ( 'NONE', *, *, #492, .F. ) ;
#21032=DIRECTION ( 'NONE',  ( 0.000000000000000000, 0.000000000000000000, 1.000000000000000000 ) ) ;
#21036=LINE ( 'NONE', #1251, #2323 ) ;
#21037=DIRECTION ( 'NONE',  ( 1.000000000000000000, 0.000000000000000000, 0.000000000000000000 ) ) ;
#21068=EDGE_CURVE ( 'NONE', #9825, #13474, #2979, .T. ) ;
#21090=DIRECTION ( 'NONE',  ( -0.8090169943749473402, 0.000000000000000000, 0.5877852522924732481 ) ) ;
#21092=LINE ( 'NONE', #11241, #2211 ) ;
#21120=EDGE_CURVE ( 'NONE', #827, #19850, #7722, .T. ) ;
#21207=ORIENTED_EDGE ( 'NONE', *, *, #15987, .T. ) ;
#21219=EDGE_CURVE ( 'NONE', #15264, #17415, #5015, .T. ) ;
#21238=CARTESIAN_POINT ( 'NONE',  ( -28.68588794268875475, 600.7448905601785327, 0.000000000000000000 ) ) ;
#21250=DIRECTION ( 'NONE',  ( 1.191790137725560488E-16, -1.000000000000000000, -0.000000000000000000 ) ) ;
#21261=DIRECTION ( 'NONE',  ( -1.000000000000000000, 0.000000000000000000, -0.000000000000000000 ) ) ;
#21270=DIRECTION ( 'NONE',  ( 0.000000000000000000, 1.000000000000000000, -0.000000000000000000 ) ) ;
#21281=CARTESIAN_POINT ( 'NONE',  ( 18.20947592957835326, 585.7448905601785327, -168.5995991907681457 ) ) ;
#21311=DIRECTION ( 'NONE',  ( 0.000000000000000000, 1.000000000000000000, -0.000000000000000000 ) ) ;
#21327=CARTESIAN_POINT ( 'NONE',  ( -28.68588794268874409, 608.2448905601786464, 0.000000000000000000 ) ) ;
#21383=EDGE_CURVE ( 'NONE', #12217, #20490, #19726, .T. ) ;
#21443=COLOUR_RGB('Off White',0.89,0.88,0.83);
#21444=FILL_AREA_STYLE_COLOUR('',#21443);
#21445=FILL_AREA_STYLE('',(#21444));
#21446=SURFACE_STYLE_FILL_AREA(#21445);
#21447=SURFACE_SIDE_STYLE('',(#21446));
#21448=SURFACE_STYLE_USAGE(.BOTH.,#21447);
#21449=PRESENTATION_STYLE_ASSIGNMENT((#21448));
ENDSEC;
END-ISO-10303-21;
